ISO-10303-21;
HEADER;
/* Generated by software containing ST-Developer
 * from STEP Tools, Inc. (www.steptools.com) 
 */

FILE_DESCRIPTION(
/* description */ (''),
/* implementation_level */ '2;1');

FILE_NAME(
/* name */ 'Configuration 1__PD8496.step',
/* time_stamp */ '2026-10-06T10:18:54-07:00',
/* author */ (''),
/* organization */ (''),
/* preprocessor_version */ 'ST-DEVELOPER v20.2',
/* originating_system */ 'Autodesk Translation Framework v15.15.0.0',
/* authorisation */ '');

FILE_SCHEMA (('AUTOMOTIVE_DESIGN { 1 0 10303 214 3 1 1 }'));
ENDSEC;

DATA;
#10=MECHANICAL_DESIGN_GEOMETRIC_PRESENTATION_REPRESENTATION('',(#82),#8445);
#64=SHAPE_REPRESENTATION_RELATIONSHIP('SRR','None',#8485,#73);
#73=ADVANCED_BREP_SHAPE_REPRESENTATION('',(#91),#8437);
#82=STYLED_ITEM('',(#8537),#91);
#91=MANIFOLD_SOLID_BREP('Body1',#4003);
#101=CONICAL_SURFACE('',#4327,0.5,0.872664625997165);
#135=CYLINDRICAL_SURFACE('',#4285,3.);
#136=CYLINDRICAL_SURFACE('',#4289,3.);
#137=CYLINDRICAL_SURFACE('',#4294,17.5);
#138=CYLINDRICAL_SURFACE('',#4300,2.99999999999999);
#139=CYLINDRICAL_SURFACE('',#4302,2.23705055212463);
#140=CYLINDRICAL_SURFACE('',#4303,17.5);
#141=CYLINDRICAL_SURFACE('',#4304,2.23705055212463);
#142=CYLINDRICAL_SURFACE('',#4306,2.99999999999999);
#143=CYLINDRICAL_SURFACE('',#4315,3.00000000000001);
#144=CYLINDRICAL_SURFACE('',#4319,2.99999999999998);
#145=CYLINDRICAL_SURFACE('',#4329,1.);
#146=CYLINDRICAL_SURFACE('',#4331,9.5);
#239=B_SPLINE_CURVE_WITH_KNOTS('',3,(#6764,#6765,#6766,#6767,#6768,#6769,
#6770),.UNSPECIFIED.,.F.,.F.,(4,1,1,1,4),(-1.,-0.785714285714286,-0.571428571428571,
-0.285714285714286,0.),.UNSPECIFIED.);
#240=B_SPLINE_CURVE_WITH_KNOTS('',3,(#6772,#6773,#6774,#6775,#6776),
 .UNSPECIFIED.,.F.,.F.,(4,1,4),(-0.801055439138956,-0.45774596523445,-2.84420950871177E-11),
 .UNSPECIFIED.);
#241=B_SPLINE_CURVE_WITH_KNOTS('',3,(#6778,#6779,#6780,#6781,#6782,#6783,
#6784,#6785,#6786,#6787,#6788,#6789,#6790,#6791,#6792,#6793,#6794,#6795,
#6796,#6797,#6798,#6799,#6800,#6801),.UNSPECIFIED.,.F.,.F.,(4,2,2,2,2,2,
2,2,2,2,2,4),(0.,0.000472673310068606,0.00105992669792163,0.00191515129472927,
0.00337317925368863,0.00606809230516856,0.0123496565483333,0.0257034558078238,
0.0532576217839337,0.110508433799565,0.205819736498927,0.232965615027244),
 .UNSPECIFIED.);
#242=B_SPLINE_CURVE_WITH_KNOTS('',3,(#6802,#6803,#6804,#6805),
 .UNSPECIFIED.,.F.,.F.,(4,4),(0.480969105510275,0.801055439138956),
 .UNSPECIFIED.);
#243=B_SPLINE_CURVE_WITH_KNOTS('',3,(#6836,#6837,#6838,#6839,#6840,#6841,
#6842),.UNSPECIFIED.,.F.,.F.,(4,1,1,1,4),(-1.,-0.785714285714286,-0.571428571428571,
-0.285714285714286,0.),.UNSPECIFIED.);
#244=B_SPLINE_CURVE_WITH_KNOTS('',3,(#6843,#6844,#6845,#6846),
 .UNSPECIFIED.,.F.,.F.,(4,4),(-2.06290888015454,-0.801055439138956),
 .UNSPECIFIED.);
#245=B_SPLINE_CURVE_WITH_KNOTS('',3,(#6847,#6848,#6849,#6850),
 .UNSPECIFIED.,.F.,.F.,(4,4),(0.801055439138956,2.06290888015454),
 .UNSPECIFIED.);
#246=B_SPLINE_CURVE_WITH_KNOTS('',3,(#6888,#6889,#6890,#6891,#6892,#6893,
#6894),.UNSPECIFIED.,.F.,.F.,(4,1,1,1,4),(-1.,-0.785714285714286,-0.571428571428571,
-0.285714285714286,0.),.UNSPECIFIED.);
#247=B_SPLINE_CURVE_WITH_KNOTS('',3,(#6895,#6896,#6897,#6898,#6899),
 .UNSPECIFIED.,.F.,.F.,(4,1,4),(-2.07918288771298,-2.069883451706,-2.06290887470076),
 .UNSPECIFIED.);
#248=B_SPLINE_CURVE_WITH_KNOTS('',3,(#6900,#6901,#6902,#6903,#6904),
 .UNSPECIFIED.,.F.,.F.,(4,1,4),(2.06290888015454,2.069883451706,2.07918288771298),
 .UNSPECIFIED.);
#249=B_SPLINE_CURVE_WITH_KNOTS('',3,(#6935,#6936,#6937,#6938,#6939,#6940,
#6941),.UNSPECIFIED.,.F.,.F.,(4,1,1,1,4),(-1.,-0.785714285714286,-0.571428571428571,
-0.285714285714286,0.),.UNSPECIFIED.);
#250=B_SPLINE_CURVE_WITH_KNOTS('',3,(#6942,#6943,#6944,#6945),
 .UNSPECIFIED.,.F.,.F.,(4,4),(-2.19760564616015,-2.07918288771299),
 .UNSPECIFIED.);
#251=B_SPLINE_CURVE_WITH_KNOTS('',3,(#6946,#6947,#6948,#6949),
 .UNSPECIFIED.,.F.,.F.,(4,4),(2.07918288771299,2.19760564616015),
 .UNSPECIFIED.);
#252=B_SPLINE_CURVE_WITH_KNOTS('',3,(#7036,#7037,#7038,#7039,#7040,#7041,
#7042),.UNSPECIFIED.,.F.,.F.,(4,1,1,1,4),(-1.,-0.785714285714286,-0.571428571428571,
-0.285714285714286,0.),.UNSPECIFIED.);
#253=B_SPLINE_CURVE_WITH_KNOTS('',3,(#7043,#7044,#7045,#7046,#7047,#7048,
#7049,#7050,#7051,#7052,#7053,#7054),.UNSPECIFIED.,.F.,.F.,(4,1,1,1,1,1,
1,1,1,4),(-7.78726759776434,-6.98874446182879,-6.19022132589323,-5.39169818995768,
-4.85934943266731,-4.59317505402212,-4.32700067537694,-3.79465191808657,
-2.99612878215101,-2.19760564621546),.UNSPECIFIED.);
#254=B_SPLINE_CURVE_WITH_KNOTS('',3,(#7055,#7056,#7057,#7058,#7059,#7060,
#7061,#7062,#7063,#7064,#7065,#7066),.UNSPECIFIED.,.F.,.F.,(4,1,1,1,1,1,
1,1,1,4),(2.19760564621546,2.99612878215101,3.79465191808657,4.32700067537694,
4.59317505402212,4.85934943266731,5.39169818995768,6.19022132589323,6.98874446182879,
7.78726759776434),.UNSPECIFIED.);
#255=B_SPLINE_CURVE_WITH_KNOTS('',3,(#7097,#7098,#7099,#7100,#7101,#7102,
#7103),.UNSPECIFIED.,.F.,.F.,(4,1,1,1,4),(-1.,-0.785714285714286,-0.571428571428571,
-0.285714285714286,0.),.UNSPECIFIED.);
#256=B_SPLINE_CURVE_WITH_KNOTS('',3,(#7104,#7105,#7106,#7107),
 .UNSPECIFIED.,.F.,.F.,(4,4),(-7.9056903551329,-7.78726759776434),
 .UNSPECIFIED.);
#257=B_SPLINE_CURVE_WITH_KNOTS('',3,(#7108,#7109,#7110,#7111),
 .UNSPECIFIED.,.F.,.F.,(4,4),(7.78726759776434,7.9056903551329),
 .UNSPECIFIED.);
#258=B_SPLINE_CURVE_WITH_KNOTS('',3,(#7149,#7150,#7151,#7152,#7153,#7154,
#7155),.UNSPECIFIED.,.F.,.F.,(4,1,1,1,4),(-1.,-0.785714285714286,-0.571428571428571,
-0.285714285714286,0.),.UNSPECIFIED.);
#259=B_SPLINE_CURVE_WITH_KNOTS('',3,(#7156,#7157,#7158,#7159,#7160),
 .UNSPECIFIED.,.F.,.F.,(4,1,4),(-7.92196437367001,-7.91266493450595,-7.90569035513291),
 .UNSPECIFIED.);
#260=B_SPLINE_CURVE_WITH_KNOTS('',3,(#7161,#7162,#7163,#7164,#7165),
 .UNSPECIFIED.,.F.,.F.,(4,1,4),(7.90569035513291,7.91266493450595,7.92196437367001),
 .UNSPECIFIED.);
#261=B_SPLINE_CURVE_WITH_KNOTS('',3,(#7196,#7197,#7198,#7199,#7200,#7201,
#7202),.UNSPECIFIED.,.F.,.F.,(4,1,1,1,4),(-1.,-0.785714285714286,-0.571428571428571,
-0.285714285714286,0.),.UNSPECIFIED.);
#262=B_SPLINE_CURVE_WITH_KNOTS('',3,(#7203,#7204,#7205,#7206),
 .UNSPECIFIED.,.F.,.F.,(4,4),(-9.18381780243075,-7.92196436821623),
 .UNSPECIFIED.);
#263=B_SPLINE_CURVE_WITH_KNOTS('',3,(#7207,#7208,#7209,#7210),
 .UNSPECIFIED.,.F.,.F.,(4,4),(7.92196437367001,9.18381780243075),
 .UNSPECIFIED.);
#264=B_SPLINE_CURVE_WITH_KNOTS('',3,(#7241,#7242,#7243,#7244,#7245,#7246,
#7247),.UNSPECIFIED.,.F.,.F.,(4,1,1,1,4),(-1.,-0.785714285714286,-0.571428571428571,
-0.285714285714286,0.),.UNSPECIFIED.);
#265=B_SPLINE_CURVE_WITH_KNOTS('',3,(#7248,#7249,#7250,#7251),
 .UNSPECIFIED.,.F.,.F.,(4,4),(-9.50411765280707,-9.18381780243075),
 .UNSPECIFIED.);
#266=B_SPLINE_CURVE_WITH_KNOTS('',3,(#7252,#7253,#7254,#7255),
 .UNSPECIFIED.,.F.,.F.,(4,4),(9.18381780243075,9.50411765280707),
 .UNSPECIFIED.);
#267=B_SPLINE_CURVE_WITH_KNOTS('',3,(#7292,#7293,#7294,#7295,#7296,#7297,
#7298,#7299,#7300,#7301,#7302,#7303,#7304,#7305,#7306,#7307,#7308,#7309),
 .UNSPECIFIED.,.F.,.F.,(4,2,2,2,2,2,2,2,4),(0.,0.106887180350865,0.224851448313138,
0.271289364363703,0.289291419641123,0.316349671609722,0.338485570421449,
0.344422245486414,0.347293667204052),.UNSPECIFIED.);
#268=B_SPLINE_CURVE_WITH_KNOTS('',3,(#7311,#7312,#7313,#7314),
 .UNSPECIFIED.,.F.,.F.,(4,4),(-0.00685019644261114,0.),.UNSPECIFIED.);
#269=B_SPLINE_CURVE_WITH_KNOTS('',3,(#7315,#7316,#7317,#7318,#7319),
 .UNSPECIFIED.,.F.,.F.,(4,1,4),(-9.98769942445863,-9.71136698388339,-9.50411765345197),
 .UNSPECIFIED.);
#270=B_SPLINE_CURVE_WITH_KNOTS('',3,(#7339,#7340,#7341,#7342),
 .UNSPECIFIED.,.F.,.F.,(4,4),(-11.987699095758,-9.98769942445863),
 .UNSPECIFIED.);
#271=B_SPLINE_CURVE_WITH_KNOTS('',3,(#7343,#7344,#7345,#7346,#7347,#7348),
 .UNSPECIFIED.,.F.,.F.,(4,2,4),(0.,1.27049294037848,2.00000006501177),
 .UNSPECIFIED.);
#272=B_SPLINE_CURVE_WITH_KNOTS('',3,(#7393,#7394,#7395,#7396,#7397,#7398,
#7399,#7400,#7401,#7402,#7403,#7404,#7405),.UNSPECIFIED.,.F.,.F.,(4,3,3,
3,4),(0.,0.0716322252392672,0.143264450478534,0.238774084130891,0.334283717783247),
 .UNSPECIFIED.);
#273=B_SPLINE_CURVE_WITH_KNOTS('',3,(#7407,#7408,#7409,#7410),
 .UNSPECIFIED.,.F.,.F.,(4,4),(-12.4397849599923,-10.3397956275468),
 .UNSPECIFIED.);
#274=B_SPLINE_CURVE_WITH_KNOTS('',3,(#7412,#7413,#7414,#7415,#7416,#7417,
#7418),.UNSPECIFIED.,.F.,.F.,(4,1,1,1,4),(0.,0.285714285714286,0.571428571428571,
0.785714285714286,1.),.UNSPECIFIED.);
#275=B_SPLINE_CURVE_WITH_KNOTS('',3,(#7419,#7420,#7421,#7422),
 .UNSPECIFIED.,.F.,.F.,(4,4),(10.3397956275468,12.4397849599923),
 .UNSPECIFIED.);
#276=B_SPLINE_CURVE_WITH_KNOTS('',3,(#7460,#7461,#7462,#7463,#7464,#7465,
#7466),.UNSPECIFIED.,.F.,.F.,(4,1,1,1,4),(-1.,-0.785714285714286,-0.571428571428571,
-0.285714285714286,0.),.UNSPECIFIED.);
#277=B_SPLINE_CURVE_WITH_KNOTS('',3,(#7467,#7468,#7469,#7470,#7471),
 .UNSPECIFIED.,.F.,.F.,(4,1,4),(10.2018503099656,10.2806762057263,10.3397956275468),
 .UNSPECIFIED.);
#278=B_SPLINE_CURVE_WITH_KNOTS('',3,(#7472,#7473,#7474,#7475,#7476),
 .UNSPECIFIED.,.F.,.F.,(4,1,4),(-10.3397956275468,-10.2806762057263,-10.2018503099656),
 .UNSPECIFIED.);
#279=B_SPLINE_CURVE_WITH_KNOTS('',3,(#7507,#7508,#7509,#7510,#7511,#7512,
#7513),.UNSPECIFIED.,.F.,.F.,(4,1,1,1,4),(0.,0.285714285714286,0.571428571428571,
0.785714285714286,1.),.UNSPECIFIED.);
#280=B_SPLINE_CURVE_WITH_KNOTS('',3,(#7514,#7515,#7516,#7517),
 .UNSPECIFIED.,.F.,.F.,(4,4),(8.93986452633385,10.2018503099635),
 .UNSPECIFIED.);
#281=B_SPLINE_CURVE_WITH_KNOTS('',3,(#7518,#7519,#7520,#7521),
 .UNSPECIFIED.,.F.,.F.,(4,4),(-10.2018503099635,-8.93986452633385),
 .UNSPECIFIED.);
#282=B_SPLINE_CURVE_WITH_KNOTS('',3,(#7559,#7560,#7561,#7562,#7563,#7564,
#7565),.UNSPECIFIED.,.F.,.F.,(4,1,1,1,4),(0.,0.285714285714286,0.571428571428571,
0.785714285714286,1.),.UNSPECIFIED.);
#283=B_SPLINE_CURVE_WITH_KNOTS('',3,(#7566,#7567,#7568,#7569,#7570),
 .UNSPECIFIED.,.F.,.F.,(4,1,4),(8.33860637357674,8.68218245774598,8.93986452087291),
 .UNSPECIFIED.);
#284=B_SPLINE_CURVE_WITH_KNOTS('',3,(#7571,#7572,#7573,#7574,#7575),
 .UNSPECIFIED.,.F.,.F.,(4,1,4),(-8.93986451541198,-8.68218245774598,-8.33860637357674),
 .UNSPECIFIED.);
#285=B_SPLINE_CURVE_WITH_KNOTS('',3,(#7648,#7649,#7650,#7651,#7652,#7653,
#7654),.UNSPECIFIED.,.F.,.F.,(4,1,1,1,4),(-1.,-0.785714285714286,-0.571428571428571,
-0.285714285714286,0.),.UNSPECIFIED.);
#286=B_SPLINE_CURVE_WITH_KNOTS('',3,(#7655,#7656,#7657,#7658,#7659,#7660,
#7661,#7662,#7663,#7664),.UNSPECIFIED.,.F.,.F.,(4,1,1,1,1,1,1,4),(4.10117860516752,
4.7065253970806,5.31187222649662,5.91721905591265,6.52256588532867,7.12791271474469,
7.73325954416072,8.33860637357674),.UNSPECIFIED.);
#287=B_SPLINE_CURVE_WITH_KNOTS('',3,(#7665,#7666,#7667,#7668,#7669,#7670,
#7671,#7672,#7673,#7674),.UNSPECIFIED.,.F.,.F.,(4,1,1,1,1,1,1,4),(-8.33860637357674,
-7.73325954416072,-7.12791271474469,-6.52256588532867,-5.91721905591265,
-5.31187222649662,-4.7065253970806,-4.10117860516752),.UNSPECIFIED.);
#288=B_SPLINE_CURVE_WITH_KNOTS('',3,(#7712,#7713,#7714,#7715,#7716,#7717,
#7718),.UNSPECIFIED.,.F.,.F.,(4,1,1,1,4),(0.,0.285714285714286,0.571428571428571,
0.785714285714286,1.),.UNSPECIFIED.);
#289=B_SPLINE_CURVE_WITH_KNOTS('',3,(#7719,#7720,#7721,#7722,#7723),
 .UNSPECIFIED.,.F.,.F.,(4,1,4),(3.4999204445805,3.75760250536717,4.10117858641605),
 .UNSPECIFIED.);
#290=B_SPLINE_CURVE_WITH_KNOTS('',3,(#7724,#7725,#7726,#7727,#7728),
 .UNSPECIFIED.,.F.,.F.,(4,1,4),(-4.10117858641605,-3.75760250536717,-3.4999204445805),
 .UNSPECIFIED.);
#291=B_SPLINE_CURVE_WITH_KNOTS('',3,(#7759,#7760,#7761,#7762,#7763,#7764,
#7765),.UNSPECIFIED.,.F.,.F.,(4,1,1,1,4),(-1.,-0.785714285714286,-0.571428571428571,
-0.285714285714286,0.),.UNSPECIFIED.);
#292=B_SPLINE_CURVE_WITH_KNOTS('',3,(#7766,#7767,#7768,#7769),
 .UNSPECIFIED.,.F.,.F.,(4,4),(2.23793465002183,3.49992043911957),
 .UNSPECIFIED.);
#293=B_SPLINE_CURVE_WITH_KNOTS('',3,(#7770,#7771,#7772,#7773),
 .UNSPECIFIED.,.F.,.F.,(4,4),(-3.49992043365863,-2.23793465002183),
 .UNSPECIFIED.);
#294=B_SPLINE_CURVE_WITH_KNOTS('',3,(#7811,#7812,#7813,#7814,#7815,#7816,
#7817),.UNSPECIFIED.,.F.,.F.,(4,1,1,1,4),(-1.,-0.785714285714286,-0.571428571428571,
-0.285714285714286,0.),.UNSPECIFIED.);
#295=B_SPLINE_CURVE_WITH_KNOTS('',3,(#7818,#7819,#7820,#7821,#7822),
 .UNSPECIFIED.,.F.,.F.,(4,1,4),(2.09998933244391,2.17881522820334,2.23793465002292),
 .UNSPECIFIED.);
#296=B_SPLINE_CURVE_WITH_KNOTS('',3,(#7823,#7824,#7825,#7826,#7827),
 .UNSPECIFIED.,.F.,.F.,(4,1,4),(-2.23793465002292,-2.17881522820334,-2.09998933244391),
 .UNSPECIFIED.);
#297=B_SPLINE_CURVE_WITH_KNOTS('',3,(#7858,#7859,#7860,#7861,#7862,#7863,
#7864,#7865,#7866,#7867,#7868,#7869,#7870),.UNSPECIFIED.,.F.,.F.,(4,3,3,
3,4),(0.,0.0716322252392673,0.143264450478534,0.238774084130891,0.334283717783247),
 .UNSPECIFIED.);
#298=B_SPLINE_CURVE_WITH_KNOTS('',3,(#7871,#7872,#7873,#7874),
 .UNSPECIFIED.,.F.,.F.,(4,4),(-1.64459338547828E-15,2.09998933244218),
 .UNSPECIFIED.);
#299=B_SPLINE_CURVE_WITH_KNOTS('',3,(#7875,#7876,#7877,#7878),
 .UNSPECIFIED.,.F.,.F.,(4,4),(-2.09998933244218,1.64459338547828E-15),
 .UNSPECIFIED.);
#317=B_SPLINE_SURFACE_WITH_KNOTS('',3,3,((#6727,#6728,#6729,#6730,#6731),
(#6732,#6733,#6734,#6735,#6736),(#6737,#6738,#6739,#6740,#6741),(#6742,
#6743,#6744,#6745,#6746),(#6747,#6748,#6749,#6750,#6751),(#6752,#6753,#6754,
#6755,#6756),(#6757,#6758,#6759,#6760,#6761)),.UNSPECIFIED.,.F.,.F.,.F.,
(4,1,1,1,4),(4,1,4),(0.,0.285714285714286,0.571428571428571,0.785714285714286,
1.),(2.84420950871177E-11,0.45774596523445,0.801055439138956),
 .UNSPECIFIED.);
#318=B_SPLINE_SURFACE_WITH_KNOTS('',3,3,((#6806,#6807,#6808,#6809),(#6810,
#6811,#6812,#6813),(#6814,#6815,#6816,#6817),(#6818,#6819,#6820,#6821),
(#6822,#6823,#6824,#6825),(#6826,#6827,#6828,#6829),(#6830,#6831,#6832,
#6833)),.UNSPECIFIED.,.F.,.F.,.F.,(4,1,1,1,4),(4,4),(0.,0.285714285714286,
0.571428571428571,0.785714285714286,1.),(0.801055439138956,2.06290888015454),
 .UNSPECIFIED.);
#319=B_SPLINE_SURFACE_WITH_KNOTS('',3,3,((#6851,#6852,#6853,#6854,#6855),
(#6856,#6857,#6858,#6859,#6860),(#6861,#6862,#6863,#6864,#6865),(#6866,
#6867,#6868,#6869,#6870),(#6871,#6872,#6873,#6874,#6875),(#6876,#6877,#6878,
#6879,#6880),(#6881,#6882,#6883,#6884,#6885)),.UNSPECIFIED.,.F.,.F.,.F.,
(4,1,1,1,4),(4,1,4),(0.,0.285714285714286,0.571428571428571,0.785714285714286,
1.),(2.06290887470076,2.069883451706,2.07918288771298),.UNSPECIFIED.);
#320=B_SPLINE_SURFACE_WITH_KNOTS('',3,3,((#6905,#6906,#6907,#6908),(#6909,
#6910,#6911,#6912),(#6913,#6914,#6915,#6916),(#6917,#6918,#6919,#6920),
(#6921,#6922,#6923,#6924),(#6925,#6926,#6927,#6928),(#6929,#6930,#6931,
#6932)),.UNSPECIFIED.,.F.,.F.,.F.,(4,1,1,1,4),(4,4),(0.,0.285714285714286,
0.571428571428571,0.785714285714286,1.),(2.07918288771299,2.19760564616015),
 .UNSPECIFIED.);
#321=B_SPLINE_SURFACE_WITH_KNOTS('',3,3,((#6950,#6951,#6952,#6953,#6954,
#6955,#6956,#6957,#6958,#6959,#6960,#6961),(#6962,#6963,#6964,#6965,#6966,
#6967,#6968,#6969,#6970,#6971,#6972,#6973),(#6974,#6975,#6976,#6977,#6978,
#6979,#6980,#6981,#6982,#6983,#6984,#6985),(#6986,#6987,#6988,#6989,#6990,
#6991,#6992,#6993,#6994,#6995,#6996,#6997),(#6998,#6999,#7000,#7001,#7002,
#7003,#7004,#7005,#7006,#7007,#7008,#7009),(#7010,#7011,#7012,#7013,#7014,
#7015,#7016,#7017,#7018,#7019,#7020,#7021),(#7022,#7023,#7024,#7025,#7026,
#7027,#7028,#7029,#7030,#7031,#7032,#7033)),.UNSPECIFIED.,.F.,.F.,.F.,(4,
1,1,1,4),(4,1,1,1,1,1,1,1,1,4),(0.,0.285714285714286,0.571428571428571,
0.785714285714286,1.),(2.19760564621546,2.99612878215101,3.79465191808657,
4.32700067537694,4.59317505402212,4.85934943266731,5.39169818995768,6.19022132589323,
6.98874446182879,7.78726759776434),.UNSPECIFIED.);
#322=B_SPLINE_SURFACE_WITH_KNOTS('',3,3,((#7067,#7068,#7069,#7070),(#7071,
#7072,#7073,#7074),(#7075,#7076,#7077,#7078),(#7079,#7080,#7081,#7082),
(#7083,#7084,#7085,#7086),(#7087,#7088,#7089,#7090),(#7091,#7092,#7093,
#7094)),.UNSPECIFIED.,.F.,.F.,.F.,(4,1,1,1,4),(4,4),(0.,0.285714285714286,
0.571428571428571,0.785714285714286,1.),(7.78726759776434,7.9056903551329),
 .UNSPECIFIED.);
#323=B_SPLINE_SURFACE_WITH_KNOTS('',3,3,((#7112,#7113,#7114,#7115,#7116),
(#7117,#7118,#7119,#7120,#7121),(#7122,#7123,#7124,#7125,#7126),(#7127,
#7128,#7129,#7130,#7131),(#7132,#7133,#7134,#7135,#7136),(#7137,#7138,#7139,
#7140,#7141),(#7142,#7143,#7144,#7145,#7146)),.UNSPECIFIED.,.F.,.F.,.F.,
(4,1,1,1,4),(4,1,4),(0.,0.285714285714286,0.571428571428571,0.785714285714286,
1.),(7.90569035513291,7.91266493450595,7.92196437367001),.UNSPECIFIED.);
#324=B_SPLINE_SURFACE_WITH_KNOTS('',3,3,((#7166,#7167,#7168,#7169),(#7170,
#7171,#7172,#7173),(#7174,#7175,#7176,#7177),(#7178,#7179,#7180,#7181),
(#7182,#7183,#7184,#7185),(#7186,#7187,#7188,#7189),(#7190,#7191,#7192,
#7193)),.UNSPECIFIED.,.F.,.F.,.F.,(4,1,1,1,4),(4,4),(0.,0.285714285714286,
0.571428571428571,0.785714285714286,1.),(7.92196436821623,9.18381780243075),
 .UNSPECIFIED.);
#325=B_SPLINE_SURFACE_WITH_KNOTS('',3,3,((#7211,#7212,#7213,#7214),(#7215,
#7216,#7217,#7218),(#7219,#7220,#7221,#7222),(#7223,#7224,#7225,#7226),
(#7227,#7228,#7229,#7230),(#7231,#7232,#7233,#7234),(#7235,#7236,#7237,
#7238)),.UNSPECIFIED.,.F.,.F.,.F.,(4,1,1,1,4),(4,4),(0.,0.285714285714286,
0.571428571428571,0.785714285714286,1.),(9.18381780243075,9.50411765280707),
 .UNSPECIFIED.);
#326=B_SPLINE_SURFACE_WITH_KNOTS('',3,3,((#7256,#7257,#7258,#7259,#7260),
(#7261,#7262,#7263,#7264,#7265),(#7266,#7267,#7268,#7269,#7270),(#7271,
#7272,#7273,#7274,#7275),(#7276,#7277,#7278,#7279,#7280),(#7281,#7282,#7283,
#7284,#7285),(#7286,#7287,#7288,#7289,#7290)),.UNSPECIFIED.,.F.,.F.,.F.,
(4,1,1,1,4),(4,1,4),(0.,0.285714285714286,0.571428571428571,0.785714285714286,
1.),(9.50411765345197,9.71136698388339,9.98769942445863),.UNSPECIFIED.);
#327=B_SPLINE_SURFACE_WITH_KNOTS('',3,3,((#7320,#7321,#7322,#7323),(#7324,
#7325,#7326,#7327),(#7328,#7329,#7330,#7331),(#7332,#7333,#7334,#7335)),
 .UNSPECIFIED.,.F.,.F.,.F.,(4,4),(4,4),(0.,0.00685219205909856),(9.98769942445863,
11.987699095758),.UNSPECIFIED.);
#328=B_SPLINE_SURFACE_WITH_KNOTS('',3,3,((#7363,#7364,#7365,#7366),(#7367,
#7368,#7369,#7370),(#7371,#7372,#7373,#7374),(#7375,#7376,#7377,#7378),
(#7379,#7380,#7381,#7382),(#7383,#7384,#7385,#7386),(#7387,#7388,#7389,
#7390)),.UNSPECIFIED.,.F.,.F.,.F.,(4,1,1,1,4),(4,4),(0.,0.285714285714286,
0.571428571428571,0.785714285714286,1.),(10.3397956275468,12.4397849599923),
 .UNSPECIFIED.);
#329=B_SPLINE_SURFACE_WITH_KNOTS('',3,3,((#7423,#7424,#7425,#7426,#7427),
(#7428,#7429,#7430,#7431,#7432),(#7433,#7434,#7435,#7436,#7437),(#7438,
#7439,#7440,#7441,#7442),(#7443,#7444,#7445,#7446,#7447),(#7448,#7449,#7450,
#7451,#7452),(#7453,#7454,#7455,#7456,#7457)),.UNSPECIFIED.,.F.,.F.,.F.,
(4,1,1,1,4),(4,1,4),(0.,0.285714285714286,0.571428571428571,0.785714285714286,
1.),(-10.3397956275468,-10.2806762057263,-10.2018503099656),
 .UNSPECIFIED.);
#330=B_SPLINE_SURFACE_WITH_KNOTS('',3,3,((#7477,#7478,#7479,#7480),(#7481,
#7482,#7483,#7484),(#7485,#7486,#7487,#7488),(#7489,#7490,#7491,#7492),
(#7493,#7494,#7495,#7496),(#7497,#7498,#7499,#7500),(#7501,#7502,#7503,
#7504)),.UNSPECIFIED.,.F.,.F.,.F.,(4,1,1,1,4),(4,4),(0.,0.285714285714286,
0.571428571428571,0.785714285714286,1.),(8.93986452633385,10.2018503099635),
 .UNSPECIFIED.);
#331=B_SPLINE_SURFACE_WITH_KNOTS('',3,3,((#7522,#7523,#7524,#7525,#7526),
(#7527,#7528,#7529,#7530,#7531),(#7532,#7533,#7534,#7535,#7536),(#7537,
#7538,#7539,#7540,#7541),(#7542,#7543,#7544,#7545,#7546),(#7547,#7548,#7549,
#7550,#7551),(#7552,#7553,#7554,#7555,#7556)),.UNSPECIFIED.,.F.,.F.,.F.,
(4,1,1,1,4),(4,1,4),(0.,0.285714285714286,0.571428571428571,0.785714285714286,
1.),(8.33860637357674,8.68218245774598,8.93986452087291),.UNSPECIFIED.);
#332=B_SPLINE_SURFACE_WITH_KNOTS('',3,3,((#7576,#7577,#7578,#7579,#7580,
#7581,#7582,#7583,#7584,#7585),(#7586,#7587,#7588,#7589,#7590,#7591,#7592,
#7593,#7594,#7595),(#7596,#7597,#7598,#7599,#7600,#7601,#7602,#7603,#7604,
#7605),(#7606,#7607,#7608,#7609,#7610,#7611,#7612,#7613,#7614,#7615),(#7616,
#7617,#7618,#7619,#7620,#7621,#7622,#7623,#7624,#7625),(#7626,#7627,#7628,
#7629,#7630,#7631,#7632,#7633,#7634,#7635),(#7636,#7637,#7638,#7639,#7640,
#7641,#7642,#7643,#7644,#7645)),.UNSPECIFIED.,.F.,.F.,.F.,(4,1,1,1,4),(4,
1,1,1,1,1,1,4),(0.,0.285714285714286,0.571428571428571,0.785714285714286,
1.),(-8.33860637357674,-7.73325954416072,-7.12791271474469,-6.52256588532867,
-5.91721905591265,-5.31187222649662,-4.7065253970806,-4.10117856766458),
 .UNSPECIFIED.);
#333=B_SPLINE_SURFACE_WITH_KNOTS('',3,3,((#7675,#7676,#7677,#7678,#7679),
(#7680,#7681,#7682,#7683,#7684),(#7685,#7686,#7687,#7688,#7689),(#7690,
#7691,#7692,#7693,#7694),(#7695,#7696,#7697,#7698,#7699),(#7700,#7701,#7702,
#7703,#7704),(#7705,#7706,#7707,#7708,#7709)),.UNSPECIFIED.,.F.,.F.,.F.,
(4,1,1,1,4),(4,1,4),(0.,0.285714285714286,0.571428571428571,0.785714285714286,
1.),(3.4999204445805,3.75760250536717,4.10117858641605),.UNSPECIFIED.);
#334=B_SPLINE_SURFACE_WITH_KNOTS('',3,3,((#7729,#7730,#7731,#7732),(#7733,
#7734,#7735,#7736),(#7737,#7738,#7739,#7740),(#7741,#7742,#7743,#7744),
(#7745,#7746,#7747,#7748),(#7749,#7750,#7751,#7752),(#7753,#7754,#7755,
#7756)),.UNSPECIFIED.,.F.,.F.,.F.,(4,1,1,1,4),(4,4),(0.,0.285714285714286,
0.571428571428571,0.785714285714286,1.),(-3.49992043911957,-2.23793465002183),
 .UNSPECIFIED.);
#335=B_SPLINE_SURFACE_WITH_KNOTS('',3,3,((#7774,#7775,#7776,#7777,#7778),
(#7779,#7780,#7781,#7782,#7783),(#7784,#7785,#7786,#7787,#7788),(#7789,
#7790,#7791,#7792,#7793),(#7794,#7795,#7796,#7797,#7798),(#7799,#7800,#7801,
#7802,#7803),(#7804,#7805,#7806,#7807,#7808)),.UNSPECIFIED.,.F.,.F.,.F.,
(4,1,1,1,4),(4,1,4),(0.,0.285714285714286,0.571428571428571,0.785714285714286,
1.),(-2.23793465002292,-2.17881522820334,-2.09998933244391),
 .UNSPECIFIED.);
#336=B_SPLINE_SURFACE_WITH_KNOTS('',3,3,((#7828,#7829,#7830,#7831),(#7832,
#7833,#7834,#7835),(#7836,#7837,#7838,#7839),(#7840,#7841,#7842,#7843),
(#7844,#7845,#7846,#7847),(#7848,#7849,#7850,#7851),(#7852,#7853,#7854,
#7855)),.UNSPECIFIED.,.F.,.F.,.F.,(4,1,1,1,4),(4,4),(0.,0.285714285714286,
0.571428571428571,0.785714285714286,1.),(-2.09998933244218,1.64459338547828E-15),
 .UNSPECIFIED.);
#348=FACE_BOUND('',#905,.T.);
#349=FACE_BOUND('',#906,.T.);
#350=FACE_BOUND('',#927,.T.);
#351=FACE_BOUND('',#928,.T.);
#441=CIRCLE('',#4286,3.);
#442=CIRCLE('',#4287,3.);
#443=CIRCLE('',#4290,3.);
#444=CIRCLE('',#4291,3.);
#445=CIRCLE('',#4295,17.5000000000459);
#446=CIRCLE('',#4296,17.5);
#447=CIRCLE('',#4299,3.00000000000001);
#448=CIRCLE('',#4307,2.99999999999999);
#449=CIRCLE('',#4309,3.00000000000001);
#450=CIRCLE('',#4316,3.00000000000001);
#451=CIRCLE('',#4317,3.00000000000001);
#452=CIRCLE('',#4320,2.99999999999998);
#453=CIRCLE('',#4321,2.99999999999998);
#454=CIRCLE('',#4328,1.);
#455=CIRCLE('',#4330,1.);
#456=CIRCLE('',#4332,9.5);
#457=CIRCLE('',#4333,9.5);
#618=FACE_OUTER_BOUND('',#864,.T.);
#619=FACE_OUTER_BOUND('',#865,.T.);
#620=FACE_OUTER_BOUND('',#866,.T.);
#621=FACE_OUTER_BOUND('',#867,.T.);
#622=FACE_OUTER_BOUND('',#868,.T.);
#623=FACE_OUTER_BOUND('',#869,.T.);
#624=FACE_OUTER_BOUND('',#870,.T.);
#625=FACE_OUTER_BOUND('',#871,.T.);
#626=FACE_OUTER_BOUND('',#872,.T.);
#627=FACE_OUTER_BOUND('',#873,.T.);
#628=FACE_OUTER_BOUND('',#874,.T.);
#629=FACE_OUTER_BOUND('',#875,.T.);
#630=FACE_OUTER_BOUND('',#876,.T.);
#631=FACE_OUTER_BOUND('',#877,.T.);
#632=FACE_OUTER_BOUND('',#878,.T.);
#633=FACE_OUTER_BOUND('',#879,.T.);
#634=FACE_OUTER_BOUND('',#880,.T.);
#635=FACE_OUTER_BOUND('',#881,.T.);
#636=FACE_OUTER_BOUND('',#882,.T.);
#637=FACE_OUTER_BOUND('',#883,.T.);
#638=FACE_OUTER_BOUND('',#884,.T.);
#639=FACE_OUTER_BOUND('',#885,.T.);
#640=FACE_OUTER_BOUND('',#886,.T.);
#641=FACE_OUTER_BOUND('',#887,.T.);
#642=FACE_OUTER_BOUND('',#888,.T.);
#643=FACE_OUTER_BOUND('',#889,.T.);
#644=FACE_OUTER_BOUND('',#890,.T.);
#645=FACE_OUTER_BOUND('',#891,.T.);
#646=FACE_OUTER_BOUND('',#892,.T.);
#647=FACE_OUTER_BOUND('',#893,.T.);
#648=FACE_OUTER_BOUND('',#894,.T.);
#649=FACE_OUTER_BOUND('',#895,.T.);
#650=FACE_OUTER_BOUND('',#896,.T.);
#651=FACE_OUTER_BOUND('',#897,.T.);
#652=FACE_OUTER_BOUND('',#898,.T.);
#653=FACE_OUTER_BOUND('',#899,.T.);
#654=FACE_OUTER_BOUND('',#900,.T.);
#655=FACE_OUTER_BOUND('',#901,.T.);
#656=FACE_OUTER_BOUND('',#902,.T.);
#657=FACE_OUTER_BOUND('',#903,.T.);
#658=FACE_OUTER_BOUND('',#904,.T.);
#659=FACE_OUTER_BOUND('',#907,.T.);
#660=FACE_OUTER_BOUND('',#908,.T.);
#661=FACE_OUTER_BOUND('',#909,.T.);
#662=FACE_OUTER_BOUND('',#910,.T.);
#663=FACE_OUTER_BOUND('',#911,.T.);
#664=FACE_OUTER_BOUND('',#912,.T.);
#665=FACE_OUTER_BOUND('',#913,.T.);
#666=FACE_OUTER_BOUND('',#914,.T.);
#667=FACE_OUTER_BOUND('',#915,.T.);
#668=FACE_OUTER_BOUND('',#916,.T.);
#669=FACE_OUTER_BOUND('',#917,.T.);
#670=FACE_OUTER_BOUND('',#918,.T.);
#671=FACE_OUTER_BOUND('',#919,.T.);
#672=FACE_OUTER_BOUND('',#920,.T.);
#673=FACE_OUTER_BOUND('',#921,.T.);
#674=FACE_OUTER_BOUND('',#922,.T.);
#675=FACE_OUTER_BOUND('',#923,.T.);
#676=FACE_OUTER_BOUND('',#924,.T.);
#677=FACE_OUTER_BOUND('',#925,.T.);
#678=FACE_OUTER_BOUND('',#926,.T.);
#679=FACE_OUTER_BOUND('',#929,.T.);
#864=EDGE_LOOP('',(#3003,#3004,#3005,#3006));
#865=EDGE_LOOP('',(#3007));
#866=EDGE_LOOP('',(#3008,#3009,#3010,#3011));
#867=EDGE_LOOP('',(#3012));
#868=EDGE_LOOP('',(#3013,#3014,#3015,#3016));
#869=EDGE_LOOP('',(#3017,#3018,#3019,#3020));
#870=EDGE_LOOP('',(#3021,#3022,#3023,#3024));
#871=EDGE_LOOP('',(#3025,#3026,#3027,#3028));
#872=EDGE_LOOP('',(#3029,#3030,#3031,#3032));
#873=EDGE_LOOP('',(#3033,#3034,#3035,#3036));
#874=EDGE_LOOP('',(#3037,#3038,#3039,#3040));
#875=EDGE_LOOP('',(#3041,#3042,#3043,#3044));
#876=EDGE_LOOP('',(#3045,#3046,#3047,#3048));
#877=EDGE_LOOP('',(#3049,#3050,#3051,#3052));
#878=EDGE_LOOP('',(#3053,#3054,#3055,#3056));
#879=EDGE_LOOP('',(#3057,#3058,#3059,#3060,#3061,#3062));
#880=EDGE_LOOP('',(#3063,#3064,#3065,#3066,#3067,#3068));
#881=EDGE_LOOP('',(#3069,#3070,#3071,#3072,#3073,#3074));
#882=EDGE_LOOP('',(#3075,#3076,#3077,#3078));
#883=EDGE_LOOP('',(#3079,#3080,#3081,#3082));
#884=EDGE_LOOP('',(#3083,#3084,#3085,#3086));
#885=EDGE_LOOP('',(#3087,#3088,#3089,#3090));
#886=EDGE_LOOP('',(#3091,#3092,#3093,#3094));
#887=EDGE_LOOP('',(#3095,#3096,#3097,#3098));
#888=EDGE_LOOP('',(#3099,#3100,#3101,#3102));
#889=EDGE_LOOP('',(#3103,#3104,#3105,#3106));
#890=EDGE_LOOP('',(#3107,#3108,#3109,#3110));
#891=EDGE_LOOP('',(#3111,#3112,#3113,#3114,#3115,#3116,#3117));
#892=EDGE_LOOP('',(#3118,#3119,#3120,#3121,#3122));
#893=EDGE_LOOP('',(#3123,#3124,#3125,#3126));
#894=EDGE_LOOP('',(#3127,#3128,#3129,#3130));
#895=EDGE_LOOP('',(#3131,#3132,#3133,#3134,#3135,#3136));
#896=EDGE_LOOP('',(#3137,#3138,#3139,#3140));
#897=EDGE_LOOP('',(#3141,#3142,#3143,#3144));
#898=EDGE_LOOP('',(#3145,#3146,#3147,#3148,#3149,#3150));
#899=EDGE_LOOP('',(#3151,#3152,#3153,#3154,#3155));
#900=EDGE_LOOP('',(#3156,#3157,#3158,#3159,#3160));
#901=EDGE_LOOP('',(#3161,#3162,#3163,#3164,#3165,#3166,#3167));
#902=EDGE_LOOP('',(#3168,#3169,#3170,#3171));
#903=EDGE_LOOP('',(#3172,#3173,#3174,#3175,#3176,#3177));
#904=EDGE_LOOP('',(#3178,#3179,#3180,#3181,#3182,#3183));
#905=EDGE_LOOP('',(#3184));
#906=EDGE_LOOP('',(#3185));
#907=EDGE_LOOP('',(#3186,#3187,#3188,#3189,#3190,#3191,#3192,#3193));
#908=EDGE_LOOP('',(#3194,#3195,#3196,#3197));
#909=EDGE_LOOP('',(#3198,#3199,#3200,#3201));
#910=EDGE_LOOP('',(#3202,#3203,#3204,#3205,#3206,#3207,#3208,#3209));
#911=EDGE_LOOP('',(#3210,#3211,#3212,#3213,#3214));
#912=EDGE_LOOP('',(#3215,#3216,#3217,#3218,#3219,#3220,#3221));
#913=EDGE_LOOP('',(#3222,#3223,#3224,#3225));
#914=EDGE_LOOP('',(#3226,#3227,#3228,#3229));
#915=EDGE_LOOP('',(#3230,#3231,#3232));
#916=EDGE_LOOP('',(#3233,#3234,#3235,#3236));
#917=EDGE_LOOP('',(#3237,#3238,#3239,#3240));
#918=EDGE_LOOP('',(#3241));
#919=EDGE_LOOP('',(#3242,#3243,#3244,#3245));
#920=EDGE_LOOP('',(#3246,#3247,#3248,#3249));
#921=EDGE_LOOP('',(#3250,#3251,#3252,#3253,#3254,#3255,#3256,#3257));
#922=EDGE_LOOP('',(#3258,#3259,#3260,#3261));
#923=EDGE_LOOP('',(#3262,#3263,#3264,#3265));
#924=EDGE_LOOP('',(#3266,#3267,#3268,#3269,#3270,#3271,#3272));
#925=EDGE_LOOP('',(#3273,#3274,#3275,#3276));
#926=EDGE_LOOP('',(#3277,#3278,#3279,#3280,#3281,#3282,#3283,#3284,#3285,
#3286,#3287,#3288,#3289,#3290,#3291,#3292,#3293,#3294,#3295,#3296,#3297,
#3298));
#927=EDGE_LOOP('',(#3299));
#928=EDGE_LOOP('',(#3300));
#929=EDGE_LOOP('',(#3301,#3302,#3303,#3304));
#1138=LINE('',#6717,#1427);
#1139=LINE('',#6724,#1428);
#1140=LINE('',#7338,#1429);
#1141=LINE('',#7351,#1430);
#1142=LINE('',#7352,#1431);
#1143=LINE('',#7355,#1432);
#1144=LINE('',#7359,#1433);
#1145=LINE('',#7362,#1434);
#1146=LINE('',#7881,#1435);
#1147=LINE('',#7884,#1436);
#1148=LINE('',#7885,#1437);
#1149=LINE('',#7887,#1438);
#1150=LINE('',#7889,#1439);
#1151=LINE('',#7891,#1440);
#1152=LINE('',#7893,#1441);
#1153=LINE('',#7895,#1442);
#1154=LINE('',#7897,#1443);
#1155=LINE('',#7900,#1444);
#1156=LINE('',#7903,#1445);
#1157=LINE('',#7906,#1446);
#1158=LINE('',#7909,#1447);
#1159=LINE('',#7912,#1448);
#1160=LINE('',#7914,#1449);
#1161=LINE('',#7915,#1450);
#1162=LINE('',#7918,#1451);
#1163=LINE('',#7919,#1452);
#1164=LINE('',#7922,#1453);
#1165=LINE('',#7923,#1454);
#1166=LINE('',#7925,#1455);
#1167=LINE('',#7927,#1456);
#1168=LINE('',#7932,#1457);
#1169=LINE('',#7935,#1458);
#1170=LINE('',#7938,#1459);
#1171=LINE('',#7940,#1460);
#1172=LINE('',#7941,#1461);
#1173=LINE('',#7946,#1462);
#1174=LINE('',#7950,#1463);
#1175=LINE('',#7952,#1464);
#1176=LINE('',#7954,#1465);
#1177=LINE('',#7956,#1466);
#1178=LINE('',#7958,#1467);
#1179=LINE('',#7960,#1468);
#1180=LINE('',#7961,#1469);
#1181=LINE('',#7964,#1470);
#1182=LINE('',#7965,#1471);
#1183=LINE('',#7968,#1472);
#1184=LINE('',#7969,#1473);
#1185=LINE('',#7972,#1474);
#1186=LINE('',#7973,#1475);
#1187=LINE('',#7976,#1476);
#1188=LINE('',#7977,#1477);
#1189=LINE('',#7982,#1478);
#1190=LINE('',#7986,#1479);
#1191=LINE('',#7991,#1480);
#1192=LINE('',#7997,#1481);
#1193=LINE('',#7999,#1482);
#1194=LINE('',#8001,#1483);
#1195=LINE('',#8002,#1484);
#1196=LINE('',#8005,#1485);
#1197=LINE('',#8007,#1486);
#1198=LINE('',#8008,#1487);
#1199=LINE('',#8011,#1488);
#1200=LINE('',#8012,#1489);
#1201=LINE('',#8014,#1490);
#1202=LINE('',#8016,#1491);
#1203=LINE('',#8017,#1492);
#1204=LINE('',#8020,#1493);
#1205=LINE('',#8021,#1494);
#1206=LINE('',#8024,#1495);
#1207=LINE('',#8025,#1496);
#1208=LINE('',#8027,#1497);
#1209=LINE('',#8029,#1498);
#1210=LINE('',#8030,#1499);
#1427=VECTOR('',#4975,3.);
#1428=VECTOR('',#4984,3.);
#1429=VECTOR('',#4989,10.);
#1430=VECTOR('',#4992,10.);
#1431=VECTOR('',#4993,10.);
#1432=VECTOR('',#4996,10.);
#1433=VECTOR('',#4999,10.);
#1434=VECTOR('',#5004,10.);
#1435=VECTOR('',#5007,10.);
#1436=VECTOR('',#5010,10.);
#1437=VECTOR('',#5011,10.);
#1438=VECTOR('',#5014,10.);
#1439=VECTOR('',#5017,10.);
#1440=VECTOR('',#5020,10.);
#1441=VECTOR('',#5023,10.);
#1442=VECTOR('',#5026,10.);
#1443=VECTOR('',#5029,10.);
#1444=VECTOR('',#5032,10.);
#1445=VECTOR('',#5035,10.);
#1446=VECTOR('',#5038,10.);
#1447=VECTOR('',#5041,10.);
#1448=VECTOR('',#5044,10.);
#1449=VECTOR('',#5045,10.);
#1450=VECTOR('',#5046,10.);
#1451=VECTOR('',#5049,10.);
#1452=VECTOR('',#5050,10.);
#1453=VECTOR('',#5053,10.);
#1454=VECTOR('',#5054,10.);
#1455=VECTOR('',#5057,10.);
#1456=VECTOR('',#5060,10.);
#1457=VECTOR('',#5065,10.);
#1458=VECTOR('',#5068,10.);
#1459=VECTOR('',#5071,10.);
#1460=VECTOR('',#5072,10.);
#1461=VECTOR('',#5073,10.);
#1462=VECTOR('',#5078,10.);
#1463=VECTOR('',#5083,10.);
#1464=VECTOR('',#5084,10.);
#1465=VECTOR('',#5085,10.);
#1466=VECTOR('',#5086,10.);
#1467=VECTOR('',#5087,10.);
#1468=VECTOR('',#5088,10.);
#1469=VECTOR('',#5089,10.);
#1470=VECTOR('',#5092,10.);
#1471=VECTOR('',#5093,10.);
#1472=VECTOR('',#5096,10.);
#1473=VECTOR('',#5097,10.);
#1474=VECTOR('',#5100,10.);
#1475=VECTOR('',#5101,10.);
#1476=VECTOR('',#5104,10.);
#1477=VECTOR('',#5105,10.);
#1478=VECTOR('',#5110,0.5);
#1479=VECTOR('',#5115,1.);
#1480=VECTOR('',#5120,9.5);
#1481=VECTOR('',#5127,10.);
#1482=VECTOR('',#5128,10.);
#1483=VECTOR('',#5129,10.);
#1484=VECTOR('',#5130,10.);
#1485=VECTOR('',#5133,10.);
#1486=VECTOR('',#5134,10.);
#1487=VECTOR('',#5135,10.);
#1488=VECTOR('',#5138,10.);
#1489=VECTOR('',#5139,10.);
#1490=VECTOR('',#5140,10.);
#1491=VECTOR('',#5141,10.);
#1492=VECTOR('',#5142,10.);
#1493=VECTOR('',#5145,10.);
#1494=VECTOR('',#5146,10.);
#1495=VECTOR('',#5149,10.);
#1496=VECTOR('',#5150,10.);
#1497=VECTOR('',#5153,10.);
#1498=VECTOR('',#5156,10.);
#1499=VECTOR('',#5157,10.);
#1753=VERTEX_POINT('',#6714);
#1754=VERTEX_POINT('',#6716);
#1755=VERTEX_POINT('',#6721);
#1756=VERTEX_POINT('',#6723);
#1757=VERTEX_POINT('',#6762);
#1758=VERTEX_POINT('',#6763);
#1759=VERTEX_POINT('',#6771);
#1760=VERTEX_POINT('',#6777);
#1761=VERTEX_POINT('',#6834);
#1762=VERTEX_POINT('',#6835);
#1763=VERTEX_POINT('',#6886);
#1764=VERTEX_POINT('',#6887);
#1765=VERTEX_POINT('',#6933);
#1766=VERTEX_POINT('',#6934);
#1767=VERTEX_POINT('',#7034);
#1768=VERTEX_POINT('',#7035);
#1769=VERTEX_POINT('',#7095);
#1770=VERTEX_POINT('',#7096);
#1771=VERTEX_POINT('',#7147);
#1772=VERTEX_POINT('',#7148);
#1773=VERTEX_POINT('',#7194);
#1774=VERTEX_POINT('',#7195);
#1775=VERTEX_POINT('',#7239);
#1776=VERTEX_POINT('',#7240);
#1777=VERTEX_POINT('',#7291);
#1778=VERTEX_POINT('',#7310);
#1779=VERTEX_POINT('',#7336);
#1780=VERTEX_POINT('',#7337);
#1781=VERTEX_POINT('',#7350);
#1782=VERTEX_POINT('',#7354);
#1783=VERTEX_POINT('',#7356);
#1784=VERTEX_POINT('',#7358);
#1785=VERTEX_POINT('',#7391);
#1786=VERTEX_POINT('',#7392);
#1787=VERTEX_POINT('',#7406);
#1788=VERTEX_POINT('',#7411);
#1789=VERTEX_POINT('',#7458);
#1790=VERTEX_POINT('',#7459);
#1791=VERTEX_POINT('',#7505);
#1792=VERTEX_POINT('',#7506);
#1793=VERTEX_POINT('',#7557);
#1794=VERTEX_POINT('',#7558);
#1795=VERTEX_POINT('',#7646);
#1796=VERTEX_POINT('',#7647);
#1797=VERTEX_POINT('',#7710);
#1798=VERTEX_POINT('',#7711);
#1799=VERTEX_POINT('',#7757);
#1800=VERTEX_POINT('',#7758);
#1801=VERTEX_POINT('',#7809);
#1802=VERTEX_POINT('',#7810);
#1803=VERTEX_POINT('',#7856);
#1804=VERTEX_POINT('',#7857);
#1805=VERTEX_POINT('',#7880);
#1806=VERTEX_POINT('',#7882);
#1807=VERTEX_POINT('',#7899);
#1808=VERTEX_POINT('',#7901);
#1809=VERTEX_POINT('',#7905);
#1810=VERTEX_POINT('',#7907);
#1811=VERTEX_POINT('',#7911);
#1812=VERTEX_POINT('',#7913);
#1813=VERTEX_POINT('',#7917);
#1814=VERTEX_POINT('',#7921);
#1815=VERTEX_POINT('',#7929);
#1816=VERTEX_POINT('',#7931);
#1817=VERTEX_POINT('',#7933);
#1818=VERTEX_POINT('',#7937);
#1819=VERTEX_POINT('',#7939);
#1820=VERTEX_POINT('',#7943);
#1821=VERTEX_POINT('',#7945);
#1822=VERTEX_POINT('',#7949);
#1823=VERTEX_POINT('',#7951);
#1824=VERTEX_POINT('',#7953);
#1825=VERTEX_POINT('',#7955);
#1826=VERTEX_POINT('',#7957);
#1827=VERTEX_POINT('',#7959);
#1828=VERTEX_POINT('',#7963);
#1829=VERTEX_POINT('',#7967);
#1830=VERTEX_POINT('',#7971);
#1831=VERTEX_POINT('',#7975);
#1832=VERTEX_POINT('',#7979);
#1833=VERTEX_POINT('',#7981);
#1834=VERTEX_POINT('',#7984);
#1835=VERTEX_POINT('',#7988);
#1836=VERTEX_POINT('',#7990);
#1837=VERTEX_POINT('',#7995);
#1838=VERTEX_POINT('',#7996);
#1839=VERTEX_POINT('',#7998);
#1840=VERTEX_POINT('',#8000);
#1841=VERTEX_POINT('',#8004);
#1842=VERTEX_POINT('',#8006);
#1843=VERTEX_POINT('',#8010);
#1844=VERTEX_POINT('',#8013);
#1845=VERTEX_POINT('',#8015);
#1846=VERTEX_POINT('',#8019);
#1847=VERTEX_POINT('',#8023);
#2202=EDGE_CURVE('',#1753,#1753,#441,.T.);
#2203=EDGE_CURVE('',#1753,#1754,#1138,.T.);
#2204=EDGE_CURVE('',#1754,#1754,#442,.T.);
#2205=EDGE_CURVE('',#1755,#1755,#443,.T.);
#2206=EDGE_CURVE('',#1755,#1756,#1139,.T.);
#2207=EDGE_CURVE('',#1756,#1756,#444,.T.);
#2208=EDGE_CURVE('',#1757,#1758,#239,.T.);
#2209=EDGE_CURVE('',#1758,#1759,#240,.T.);
#2210=EDGE_CURVE('',#1759,#1760,#241,.T.);
#2211=EDGE_CURVE('',#1760,#1757,#242,.T.);
#2212=EDGE_CURVE('',#1761,#1762,#243,.T.);
#2213=EDGE_CURVE('',#1762,#1758,#244,.T.);
#2214=EDGE_CURVE('',#1757,#1761,#245,.T.);
#2215=EDGE_CURVE('',#1763,#1764,#246,.T.);
#2216=EDGE_CURVE('',#1764,#1762,#247,.T.);
#2217=EDGE_CURVE('',#1761,#1763,#248,.T.);
#2218=EDGE_CURVE('',#1765,#1766,#249,.T.);
#2219=EDGE_CURVE('',#1766,#1764,#250,.T.);
#2220=EDGE_CURVE('',#1763,#1765,#251,.T.);
#2221=EDGE_CURVE('',#1767,#1768,#252,.T.);
#2222=EDGE_CURVE('',#1768,#1766,#253,.T.);
#2223=EDGE_CURVE('',#1765,#1767,#254,.T.);
#2224=EDGE_CURVE('',#1769,#1770,#255,.T.);
#2225=EDGE_CURVE('',#1770,#1768,#256,.T.);
#2226=EDGE_CURVE('',#1767,#1769,#257,.T.);
#2227=EDGE_CURVE('',#1771,#1772,#258,.T.);
#2228=EDGE_CURVE('',#1772,#1770,#259,.T.);
#2229=EDGE_CURVE('',#1769,#1771,#260,.T.);
#2230=EDGE_CURVE('',#1773,#1774,#261,.T.);
#2231=EDGE_CURVE('',#1774,#1772,#262,.T.);
#2232=EDGE_CURVE('',#1771,#1773,#263,.T.);
#2233=EDGE_CURVE('',#1775,#1776,#264,.T.);
#2234=EDGE_CURVE('',#1776,#1774,#265,.T.);
#2235=EDGE_CURVE('',#1773,#1775,#266,.T.);
#2236=EDGE_CURVE('',#1775,#1777,#267,.T.);
#2237=EDGE_CURVE('',#1777,#1778,#268,.T.);
#2238=EDGE_CURVE('',#1778,#1776,#269,.T.);
#2239=EDGE_CURVE('',#1779,#1780,#1140,.T.);
#2240=EDGE_CURVE('',#1779,#1778,#270,.T.);
#2241=EDGE_CURVE('',#1777,#1780,#271,.T.);
#2242=EDGE_CURVE('',#1781,#1767,#1141,.T.);
#2243=EDGE_CURVE('',#1781,#1775,#1142,.T.);
#2244=EDGE_CURVE('',#1765,#1782,#1143,.T.);
#2245=EDGE_CURVE('',#1782,#1783,#445,.T.);
#2246=EDGE_CURVE('',#1783,#1784,#1144,.T.);
#2247=EDGE_CURVE('',#1784,#1781,#446,.T.);
#2248=EDGE_CURVE('',#1760,#1782,#1145,.T.);
#2249=EDGE_CURVE('',#1785,#1786,#272,.T.);
#2250=EDGE_CURVE('',#1786,#1787,#273,.T.);
#2251=EDGE_CURVE('',#1787,#1788,#274,.T.);
#2252=EDGE_CURVE('',#1788,#1785,#275,.T.);
#2253=EDGE_CURVE('',#1789,#1790,#276,.T.);
#2254=EDGE_CURVE('',#1790,#1788,#277,.T.);
#2255=EDGE_CURVE('',#1787,#1789,#278,.T.);
#2256=EDGE_CURVE('',#1791,#1792,#279,.T.);
#2257=EDGE_CURVE('',#1792,#1790,#280,.T.);
#2258=EDGE_CURVE('',#1789,#1791,#281,.T.);
#2259=EDGE_CURVE('',#1793,#1794,#282,.T.);
#2260=EDGE_CURVE('',#1794,#1792,#283,.T.);
#2261=EDGE_CURVE('',#1791,#1793,#284,.T.);
#2262=EDGE_CURVE('',#1795,#1796,#285,.T.);
#2263=EDGE_CURVE('',#1796,#1794,#286,.T.);
#2264=EDGE_CURVE('',#1793,#1795,#287,.T.);
#2265=EDGE_CURVE('',#1797,#1798,#288,.T.);
#2266=EDGE_CURVE('',#1798,#1796,#289,.T.);
#2267=EDGE_CURVE('',#1795,#1797,#290,.T.);
#2268=EDGE_CURVE('',#1799,#1800,#291,.T.);
#2269=EDGE_CURVE('',#1800,#1798,#292,.T.);
#2270=EDGE_CURVE('',#1797,#1799,#293,.T.);
#2271=EDGE_CURVE('',#1801,#1802,#294,.T.);
#2272=EDGE_CURVE('',#1802,#1800,#295,.T.);
#2273=EDGE_CURVE('',#1799,#1801,#296,.T.);
#2274=EDGE_CURVE('',#1803,#1804,#297,.T.);
#2275=EDGE_CURVE('',#1804,#1802,#298,.T.);
#2276=EDGE_CURVE('',#1801,#1803,#299,.T.);
#2277=EDGE_CURVE('',#1780,#1805,#1146,.T.);
#2278=EDGE_CURVE('',#1805,#1806,#447,.T.);
#2279=EDGE_CURVE('',#1803,#1806,#1147,.T.);
#2280=EDGE_CURVE('',#1801,#1778,#1148,.T.);
#2281=EDGE_CURVE('',#1799,#1774,#1149,.T.);
#2282=EDGE_CURVE('',#1797,#1772,#1150,.T.);
#2283=EDGE_CURVE('',#1795,#1770,#1151,.T.);
#2284=EDGE_CURVE('',#1793,#1764,#1152,.T.);
#2285=EDGE_CURVE('',#1791,#1762,#1153,.T.);
#2286=EDGE_CURVE('',#1789,#1758,#1154,.T.);
#2287=EDGE_CURVE('',#1787,#1807,#1155,.T.);
#2288=EDGE_CURVE('',#1807,#1808,#448,.T.);
#2289=EDGE_CURVE('',#1808,#1759,#1156,.T.);
#2290=EDGE_CURVE('',#1786,#1809,#1157,.T.);
#2291=EDGE_CURVE('',#1809,#1810,#449,.T.);
#2292=EDGE_CURVE('',#1810,#1807,#1158,.T.);
#2293=EDGE_CURVE('',#1811,#1785,#1159,.T.);
#2294=EDGE_CURVE('',#1811,#1812,#1160,.T.);
#2295=EDGE_CURVE('',#1812,#1809,#1161,.T.);
#2296=EDGE_CURVE('',#1813,#1784,#1162,.T.);
#2297=EDGE_CURVE('',#1813,#1805,#1163,.T.);
#2298=EDGE_CURVE('',#1814,#1783,#1164,.T.);
#2299=EDGE_CURVE('',#1813,#1814,#1165,.T.);
#2300=EDGE_CURVE('',#1814,#1808,#1166,.T.);
#2301=EDGE_CURVE('',#1810,#1805,#1167,.T.);
#2302=EDGE_CURVE('',#1815,#1812,#450,.T.);
#2303=EDGE_CURVE('',#1815,#1816,#1168,.T.);
#2304=EDGE_CURVE('',#1817,#1816,#451,.T.);
#2305=EDGE_CURVE('',#1806,#1817,#1169,.T.);
#2306=EDGE_CURVE('',#1818,#1815,#1170,.T.);
#2307=EDGE_CURVE('',#1818,#1819,#1171,.T.);
#2308=EDGE_CURVE('',#1816,#1819,#1172,.T.);
#2309=EDGE_CURVE('',#1820,#1818,#452,.T.);
#2310=EDGE_CURVE('',#1820,#1821,#1173,.T.);
#2311=EDGE_CURVE('',#1819,#1821,#453,.T.);
#2312=EDGE_CURVE('',#1822,#1820,#1174,.T.);
#2313=EDGE_CURVE('',#1823,#1822,#1175,.T.);
#2314=EDGE_CURVE('',#1824,#1823,#1176,.T.);
#2315=EDGE_CURVE('',#1824,#1825,#1177,.T.);
#2316=EDGE_CURVE('',#1826,#1825,#1178,.T.);
#2317=EDGE_CURVE('',#1827,#1826,#1179,.T.);
#2318=EDGE_CURVE('',#1821,#1827,#1180,.T.);
#2319=EDGE_CURVE('',#1828,#1817,#1181,.T.);
#2320=EDGE_CURVE('',#1828,#1804,#1182,.T.);
#2321=EDGE_CURVE('',#1829,#1827,#1183,.T.);
#2322=EDGE_CURVE('',#1829,#1828,#1184,.T.);
#2323=EDGE_CURVE('',#1830,#1826,#1185,.T.);
#2324=EDGE_CURVE('',#1830,#1829,#1186,.T.);
#2325=EDGE_CURVE('',#1831,#1825,#1187,.T.);
#2326=EDGE_CURVE('',#1831,#1830,#1188,.T.);
#2327=EDGE_CURVE('',#1832,#1832,#454,.T.);
#2328=EDGE_CURVE('',#1832,#1833,#1189,.T.);
#2329=EDGE_CURVE('',#1834,#1834,#455,.T.);
#2330=EDGE_CURVE('',#1834,#1832,#1190,.T.);
#2331=EDGE_CURVE('',#1835,#1835,#456,.T.);
#2332=EDGE_CURVE('',#1835,#1836,#1191,.T.);
#2333=EDGE_CURVE('',#1836,#1836,#457,.T.);
#2334=EDGE_CURVE('',#1837,#1838,#1192,.T.);
#2335=EDGE_CURVE('',#1837,#1839,#1193,.T.);
#2336=EDGE_CURVE('',#1840,#1839,#1194,.T.);
#2337=EDGE_CURVE('',#1838,#1840,#1195,.T.);
#2338=EDGE_CURVE('',#1838,#1841,#1196,.T.);
#2339=EDGE_CURVE('',#1842,#1840,#1197,.T.);
#2340=EDGE_CURVE('',#1841,#1842,#1198,.T.);
#2341=EDGE_CURVE('',#1843,#1824,#1199,.T.);
#2342=EDGE_CURVE('',#1841,#1843,#1200,.T.);
#2343=EDGE_CURVE('',#1844,#1842,#1201,.T.);
#2344=EDGE_CURVE('',#1845,#1844,#1202,.T.);
#2345=EDGE_CURVE('',#1845,#1831,#1203,.T.);
#2346=EDGE_CURVE('',#1846,#1823,#1204,.T.);
#2347=EDGE_CURVE('',#1843,#1846,#1205,.T.);
#2348=EDGE_CURVE('',#1847,#1822,#1206,.T.);
#2349=EDGE_CURVE('',#1846,#1847,#1207,.T.);
#2350=EDGE_CURVE('',#1847,#1811,#1208,.T.);
#2351=EDGE_CURVE('',#1837,#1845,#1209,.T.);
#2352=EDGE_CURVE('',#1839,#1844,#1210,.T.);
#3003=ORIENTED_EDGE('',*,*,#2202,.F.);
#3004=ORIENTED_EDGE('',*,*,#2203,.T.);
#3005=ORIENTED_EDGE('',*,*,#2204,.T.);
#3006=ORIENTED_EDGE('',*,*,#2203,.F.);
#3007=ORIENTED_EDGE('',*,*,#2204,.F.);
#3008=ORIENTED_EDGE('',*,*,#2205,.F.);
#3009=ORIENTED_EDGE('',*,*,#2206,.T.);
#3010=ORIENTED_EDGE('',*,*,#2207,.T.);
#3011=ORIENTED_EDGE('',*,*,#2206,.F.);
#3012=ORIENTED_EDGE('',*,*,#2207,.F.);
#3013=ORIENTED_EDGE('',*,*,#2208,.T.);
#3014=ORIENTED_EDGE('',*,*,#2209,.T.);
#3015=ORIENTED_EDGE('',*,*,#2210,.T.);
#3016=ORIENTED_EDGE('',*,*,#2211,.T.);
#3017=ORIENTED_EDGE('',*,*,#2212,.T.);
#3018=ORIENTED_EDGE('',*,*,#2213,.T.);
#3019=ORIENTED_EDGE('',*,*,#2208,.F.);
#3020=ORIENTED_EDGE('',*,*,#2214,.T.);
#3021=ORIENTED_EDGE('',*,*,#2215,.T.);
#3022=ORIENTED_EDGE('',*,*,#2216,.T.);
#3023=ORIENTED_EDGE('',*,*,#2212,.F.);
#3024=ORIENTED_EDGE('',*,*,#2217,.T.);
#3025=ORIENTED_EDGE('',*,*,#2218,.T.);
#3026=ORIENTED_EDGE('',*,*,#2219,.T.);
#3027=ORIENTED_EDGE('',*,*,#2215,.F.);
#3028=ORIENTED_EDGE('',*,*,#2220,.T.);
#3029=ORIENTED_EDGE('',*,*,#2221,.T.);
#3030=ORIENTED_EDGE('',*,*,#2222,.T.);
#3031=ORIENTED_EDGE('',*,*,#2218,.F.);
#3032=ORIENTED_EDGE('',*,*,#2223,.T.);
#3033=ORIENTED_EDGE('',*,*,#2224,.T.);
#3034=ORIENTED_EDGE('',*,*,#2225,.T.);
#3035=ORIENTED_EDGE('',*,*,#2221,.F.);
#3036=ORIENTED_EDGE('',*,*,#2226,.T.);
#3037=ORIENTED_EDGE('',*,*,#2227,.T.);
#3038=ORIENTED_EDGE('',*,*,#2228,.T.);
#3039=ORIENTED_EDGE('',*,*,#2224,.F.);
#3040=ORIENTED_EDGE('',*,*,#2229,.T.);
#3041=ORIENTED_EDGE('',*,*,#2230,.T.);
#3042=ORIENTED_EDGE('',*,*,#2231,.T.);
#3043=ORIENTED_EDGE('',*,*,#2227,.F.);
#3044=ORIENTED_EDGE('',*,*,#2232,.T.);
#3045=ORIENTED_EDGE('',*,*,#2233,.T.);
#3046=ORIENTED_EDGE('',*,*,#2234,.T.);
#3047=ORIENTED_EDGE('',*,*,#2230,.F.);
#3048=ORIENTED_EDGE('',*,*,#2235,.T.);
#3049=ORIENTED_EDGE('',*,*,#2236,.T.);
#3050=ORIENTED_EDGE('',*,*,#2237,.T.);
#3051=ORIENTED_EDGE('',*,*,#2238,.T.);
#3052=ORIENTED_EDGE('',*,*,#2233,.F.);
#3053=ORIENTED_EDGE('',*,*,#2239,.F.);
#3054=ORIENTED_EDGE('',*,*,#2240,.T.);
#3055=ORIENTED_EDGE('',*,*,#2237,.F.);
#3056=ORIENTED_EDGE('',*,*,#2241,.T.);
#3057=ORIENTED_EDGE('',*,*,#2235,.F.);
#3058=ORIENTED_EDGE('',*,*,#2232,.F.);
#3059=ORIENTED_EDGE('',*,*,#2229,.F.);
#3060=ORIENTED_EDGE('',*,*,#2226,.F.);
#3061=ORIENTED_EDGE('',*,*,#2242,.F.);
#3062=ORIENTED_EDGE('',*,*,#2243,.T.);
#3063=ORIENTED_EDGE('',*,*,#2223,.F.);
#3064=ORIENTED_EDGE('',*,*,#2244,.T.);
#3065=ORIENTED_EDGE('',*,*,#2245,.T.);
#3066=ORIENTED_EDGE('',*,*,#2246,.T.);
#3067=ORIENTED_EDGE('',*,*,#2247,.T.);
#3068=ORIENTED_EDGE('',*,*,#2242,.T.);
#3069=ORIENTED_EDGE('',*,*,#2220,.F.);
#3070=ORIENTED_EDGE('',*,*,#2217,.F.);
#3071=ORIENTED_EDGE('',*,*,#2214,.F.);
#3072=ORIENTED_EDGE('',*,*,#2211,.F.);
#3073=ORIENTED_EDGE('',*,*,#2248,.T.);
#3074=ORIENTED_EDGE('',*,*,#2244,.F.);
#3075=ORIENTED_EDGE('',*,*,#2249,.T.);
#3076=ORIENTED_EDGE('',*,*,#2250,.T.);
#3077=ORIENTED_EDGE('',*,*,#2251,.T.);
#3078=ORIENTED_EDGE('',*,*,#2252,.T.);
#3079=ORIENTED_EDGE('',*,*,#2253,.T.);
#3080=ORIENTED_EDGE('',*,*,#2254,.T.);
#3081=ORIENTED_EDGE('',*,*,#2251,.F.);
#3082=ORIENTED_EDGE('',*,*,#2255,.T.);
#3083=ORIENTED_EDGE('',*,*,#2256,.T.);
#3084=ORIENTED_EDGE('',*,*,#2257,.T.);
#3085=ORIENTED_EDGE('',*,*,#2253,.F.);
#3086=ORIENTED_EDGE('',*,*,#2258,.T.);
#3087=ORIENTED_EDGE('',*,*,#2259,.T.);
#3088=ORIENTED_EDGE('',*,*,#2260,.T.);
#3089=ORIENTED_EDGE('',*,*,#2256,.F.);
#3090=ORIENTED_EDGE('',*,*,#2261,.T.);
#3091=ORIENTED_EDGE('',*,*,#2262,.T.);
#3092=ORIENTED_EDGE('',*,*,#2263,.T.);
#3093=ORIENTED_EDGE('',*,*,#2259,.F.);
#3094=ORIENTED_EDGE('',*,*,#2264,.T.);
#3095=ORIENTED_EDGE('',*,*,#2265,.T.);
#3096=ORIENTED_EDGE('',*,*,#2266,.T.);
#3097=ORIENTED_EDGE('',*,*,#2262,.F.);
#3098=ORIENTED_EDGE('',*,*,#2267,.T.);
#3099=ORIENTED_EDGE('',*,*,#2268,.T.);
#3100=ORIENTED_EDGE('',*,*,#2269,.T.);
#3101=ORIENTED_EDGE('',*,*,#2265,.F.);
#3102=ORIENTED_EDGE('',*,*,#2270,.T.);
#3103=ORIENTED_EDGE('',*,*,#2271,.T.);
#3104=ORIENTED_EDGE('',*,*,#2272,.T.);
#3105=ORIENTED_EDGE('',*,*,#2268,.F.);
#3106=ORIENTED_EDGE('',*,*,#2273,.T.);
#3107=ORIENTED_EDGE('',*,*,#2274,.T.);
#3108=ORIENTED_EDGE('',*,*,#2275,.T.);
#3109=ORIENTED_EDGE('',*,*,#2271,.F.);
#3110=ORIENTED_EDGE('',*,*,#2276,.T.);
#3111=ORIENTED_EDGE('',*,*,#2239,.T.);
#3112=ORIENTED_EDGE('',*,*,#2277,.T.);
#3113=ORIENTED_EDGE('',*,*,#2278,.T.);
#3114=ORIENTED_EDGE('',*,*,#2279,.F.);
#3115=ORIENTED_EDGE('',*,*,#2276,.F.);
#3116=ORIENTED_EDGE('',*,*,#2280,.T.);
#3117=ORIENTED_EDGE('',*,*,#2240,.F.);
#3118=ORIENTED_EDGE('',*,*,#2238,.F.);
#3119=ORIENTED_EDGE('',*,*,#2280,.F.);
#3120=ORIENTED_EDGE('',*,*,#2273,.F.);
#3121=ORIENTED_EDGE('',*,*,#2281,.T.);
#3122=ORIENTED_EDGE('',*,*,#2234,.F.);
#3123=ORIENTED_EDGE('',*,*,#2231,.F.);
#3124=ORIENTED_EDGE('',*,*,#2281,.F.);
#3125=ORIENTED_EDGE('',*,*,#2270,.F.);
#3126=ORIENTED_EDGE('',*,*,#2282,.T.);
#3127=ORIENTED_EDGE('',*,*,#2228,.F.);
#3128=ORIENTED_EDGE('',*,*,#2282,.F.);
#3129=ORIENTED_EDGE('',*,*,#2267,.F.);
#3130=ORIENTED_EDGE('',*,*,#2283,.T.);
#3131=ORIENTED_EDGE('',*,*,#2225,.F.);
#3132=ORIENTED_EDGE('',*,*,#2283,.F.);
#3133=ORIENTED_EDGE('',*,*,#2264,.F.);
#3134=ORIENTED_EDGE('',*,*,#2284,.T.);
#3135=ORIENTED_EDGE('',*,*,#2219,.F.);
#3136=ORIENTED_EDGE('',*,*,#2222,.F.);
#3137=ORIENTED_EDGE('',*,*,#2216,.F.);
#3138=ORIENTED_EDGE('',*,*,#2284,.F.);
#3139=ORIENTED_EDGE('',*,*,#2261,.F.);
#3140=ORIENTED_EDGE('',*,*,#2285,.T.);
#3141=ORIENTED_EDGE('',*,*,#2213,.F.);
#3142=ORIENTED_EDGE('',*,*,#2285,.F.);
#3143=ORIENTED_EDGE('',*,*,#2258,.F.);
#3144=ORIENTED_EDGE('',*,*,#2286,.T.);
#3145=ORIENTED_EDGE('',*,*,#2209,.F.);
#3146=ORIENTED_EDGE('',*,*,#2286,.F.);
#3147=ORIENTED_EDGE('',*,*,#2255,.F.);
#3148=ORIENTED_EDGE('',*,*,#2287,.T.);
#3149=ORIENTED_EDGE('',*,*,#2288,.T.);
#3150=ORIENTED_EDGE('',*,*,#2289,.T.);
#3151=ORIENTED_EDGE('',*,*,#2250,.F.);
#3152=ORIENTED_EDGE('',*,*,#2290,.T.);
#3153=ORIENTED_EDGE('',*,*,#2291,.T.);
#3154=ORIENTED_EDGE('',*,*,#2292,.T.);
#3155=ORIENTED_EDGE('',*,*,#2287,.F.);
#3156=ORIENTED_EDGE('',*,*,#2249,.F.);
#3157=ORIENTED_EDGE('',*,*,#2293,.F.);
#3158=ORIENTED_EDGE('',*,*,#2294,.T.);
#3159=ORIENTED_EDGE('',*,*,#2295,.T.);
#3160=ORIENTED_EDGE('',*,*,#2290,.F.);
#3161=ORIENTED_EDGE('',*,*,#2247,.F.);
#3162=ORIENTED_EDGE('',*,*,#2296,.F.);
#3163=ORIENTED_EDGE('',*,*,#2297,.T.);
#3164=ORIENTED_EDGE('',*,*,#2277,.F.);
#3165=ORIENTED_EDGE('',*,*,#2241,.F.);
#3166=ORIENTED_EDGE('',*,*,#2236,.F.);
#3167=ORIENTED_EDGE('',*,*,#2243,.F.);
#3168=ORIENTED_EDGE('',*,*,#2246,.F.);
#3169=ORIENTED_EDGE('',*,*,#2298,.F.);
#3170=ORIENTED_EDGE('',*,*,#2299,.F.);
#3171=ORIENTED_EDGE('',*,*,#2296,.T.);
#3172=ORIENTED_EDGE('',*,*,#2245,.F.);
#3173=ORIENTED_EDGE('',*,*,#2248,.F.);
#3174=ORIENTED_EDGE('',*,*,#2210,.F.);
#3175=ORIENTED_EDGE('',*,*,#2289,.F.);
#3176=ORIENTED_EDGE('',*,*,#2300,.F.);
#3177=ORIENTED_EDGE('',*,*,#2298,.T.);
#3178=ORIENTED_EDGE('',*,*,#2297,.F.);
#3179=ORIENTED_EDGE('',*,*,#2299,.T.);
#3180=ORIENTED_EDGE('',*,*,#2300,.T.);
#3181=ORIENTED_EDGE('',*,*,#2288,.F.);
#3182=ORIENTED_EDGE('',*,*,#2292,.F.);
#3183=ORIENTED_EDGE('',*,*,#2301,.T.);
#3184=ORIENTED_EDGE('',*,*,#2202,.T.);
#3185=ORIENTED_EDGE('',*,*,#2205,.T.);
#3186=ORIENTED_EDGE('',*,*,#2291,.F.);
#3187=ORIENTED_EDGE('',*,*,#2295,.F.);
#3188=ORIENTED_EDGE('',*,*,#2302,.F.);
#3189=ORIENTED_EDGE('',*,*,#2303,.T.);
#3190=ORIENTED_EDGE('',*,*,#2304,.F.);
#3191=ORIENTED_EDGE('',*,*,#2305,.F.);
#3192=ORIENTED_EDGE('',*,*,#2278,.F.);
#3193=ORIENTED_EDGE('',*,*,#2301,.F.);
#3194=ORIENTED_EDGE('',*,*,#2306,.F.);
#3195=ORIENTED_EDGE('',*,*,#2307,.T.);
#3196=ORIENTED_EDGE('',*,*,#2308,.F.);
#3197=ORIENTED_EDGE('',*,*,#2303,.F.);
#3198=ORIENTED_EDGE('',*,*,#2309,.F.);
#3199=ORIENTED_EDGE('',*,*,#2310,.T.);
#3200=ORIENTED_EDGE('',*,*,#2311,.F.);
#3201=ORIENTED_EDGE('',*,*,#2307,.F.);
#3202=ORIENTED_EDGE('',*,*,#2312,.F.);
#3203=ORIENTED_EDGE('',*,*,#2313,.F.);
#3204=ORIENTED_EDGE('',*,*,#2314,.F.);
#3205=ORIENTED_EDGE('',*,*,#2315,.T.);
#3206=ORIENTED_EDGE('',*,*,#2316,.F.);
#3207=ORIENTED_EDGE('',*,*,#2317,.F.);
#3208=ORIENTED_EDGE('',*,*,#2318,.F.);
#3209=ORIENTED_EDGE('',*,*,#2310,.F.);
#3210=ORIENTED_EDGE('',*,*,#2274,.F.);
#3211=ORIENTED_EDGE('',*,*,#2279,.T.);
#3212=ORIENTED_EDGE('',*,*,#2305,.T.);
#3213=ORIENTED_EDGE('',*,*,#2319,.F.);
#3214=ORIENTED_EDGE('',*,*,#2320,.T.);
#3215=ORIENTED_EDGE('',*,*,#2304,.T.);
#3216=ORIENTED_EDGE('',*,*,#2308,.T.);
#3217=ORIENTED_EDGE('',*,*,#2311,.T.);
#3218=ORIENTED_EDGE('',*,*,#2318,.T.);
#3219=ORIENTED_EDGE('',*,*,#2321,.F.);
#3220=ORIENTED_EDGE('',*,*,#2322,.T.);
#3221=ORIENTED_EDGE('',*,*,#2319,.T.);
#3222=ORIENTED_EDGE('',*,*,#2317,.T.);
#3223=ORIENTED_EDGE('',*,*,#2323,.F.);
#3224=ORIENTED_EDGE('',*,*,#2324,.T.);
#3225=ORIENTED_EDGE('',*,*,#2321,.T.);
#3226=ORIENTED_EDGE('',*,*,#2316,.T.);
#3227=ORIENTED_EDGE('',*,*,#2325,.F.);
#3228=ORIENTED_EDGE('',*,*,#2326,.T.);
#3229=ORIENTED_EDGE('',*,*,#2323,.T.);
#3230=ORIENTED_EDGE('',*,*,#2327,.F.);
#3231=ORIENTED_EDGE('',*,*,#2328,.T.);
#3232=ORIENTED_EDGE('',*,*,#2328,.F.);
#3233=ORIENTED_EDGE('',*,*,#2329,.F.);
#3234=ORIENTED_EDGE('',*,*,#2330,.T.);
#3235=ORIENTED_EDGE('',*,*,#2327,.T.);
#3236=ORIENTED_EDGE('',*,*,#2330,.F.);
#3237=ORIENTED_EDGE('',*,*,#2331,.F.);
#3238=ORIENTED_EDGE('',*,*,#2332,.T.);
#3239=ORIENTED_EDGE('',*,*,#2333,.T.);
#3240=ORIENTED_EDGE('',*,*,#2332,.F.);
#3241=ORIENTED_EDGE('',*,*,#2333,.F.);
#3242=ORIENTED_EDGE('',*,*,#2334,.F.);
#3243=ORIENTED_EDGE('',*,*,#2335,.T.);
#3244=ORIENTED_EDGE('',*,*,#2336,.F.);
#3245=ORIENTED_EDGE('',*,*,#2337,.F.);
#3246=ORIENTED_EDGE('',*,*,#2338,.F.);
#3247=ORIENTED_EDGE('',*,*,#2337,.T.);
#3248=ORIENTED_EDGE('',*,*,#2339,.F.);
#3249=ORIENTED_EDGE('',*,*,#2340,.F.);
#3250=ORIENTED_EDGE('',*,*,#2341,.F.);
#3251=ORIENTED_EDGE('',*,*,#2342,.F.);
#3252=ORIENTED_EDGE('',*,*,#2340,.T.);
#3253=ORIENTED_EDGE('',*,*,#2343,.F.);
#3254=ORIENTED_EDGE('',*,*,#2344,.F.);
#3255=ORIENTED_EDGE('',*,*,#2345,.T.);
#3256=ORIENTED_EDGE('',*,*,#2325,.T.);
#3257=ORIENTED_EDGE('',*,*,#2315,.F.);
#3258=ORIENTED_EDGE('',*,*,#2314,.T.);
#3259=ORIENTED_EDGE('',*,*,#2346,.F.);
#3260=ORIENTED_EDGE('',*,*,#2347,.F.);
#3261=ORIENTED_EDGE('',*,*,#2341,.T.);
#3262=ORIENTED_EDGE('',*,*,#2313,.T.);
#3263=ORIENTED_EDGE('',*,*,#2348,.F.);
#3264=ORIENTED_EDGE('',*,*,#2349,.F.);
#3265=ORIENTED_EDGE('',*,*,#2346,.T.);
#3266=ORIENTED_EDGE('',*,*,#2302,.T.);
#3267=ORIENTED_EDGE('',*,*,#2294,.F.);
#3268=ORIENTED_EDGE('',*,*,#2350,.F.);
#3269=ORIENTED_EDGE('',*,*,#2348,.T.);
#3270=ORIENTED_EDGE('',*,*,#2312,.T.);
#3271=ORIENTED_EDGE('',*,*,#2309,.T.);
#3272=ORIENTED_EDGE('',*,*,#2306,.T.);
#3273=ORIENTED_EDGE('',*,*,#2351,.T.);
#3274=ORIENTED_EDGE('',*,*,#2344,.T.);
#3275=ORIENTED_EDGE('',*,*,#2352,.F.);
#3276=ORIENTED_EDGE('',*,*,#2335,.F.);
#3277=ORIENTED_EDGE('',*,*,#2275,.F.);
#3278=ORIENTED_EDGE('',*,*,#2320,.F.);
#3279=ORIENTED_EDGE('',*,*,#2322,.F.);
#3280=ORIENTED_EDGE('',*,*,#2324,.F.);
#3281=ORIENTED_EDGE('',*,*,#2326,.F.);
#3282=ORIENTED_EDGE('',*,*,#2345,.F.);
#3283=ORIENTED_EDGE('',*,*,#2351,.F.);
#3284=ORIENTED_EDGE('',*,*,#2334,.T.);
#3285=ORIENTED_EDGE('',*,*,#2338,.T.);
#3286=ORIENTED_EDGE('',*,*,#2342,.T.);
#3287=ORIENTED_EDGE('',*,*,#2347,.T.);
#3288=ORIENTED_EDGE('',*,*,#2349,.T.);
#3289=ORIENTED_EDGE('',*,*,#2350,.T.);
#3290=ORIENTED_EDGE('',*,*,#2293,.T.);
#3291=ORIENTED_EDGE('',*,*,#2252,.F.);
#3292=ORIENTED_EDGE('',*,*,#2254,.F.);
#3293=ORIENTED_EDGE('',*,*,#2257,.F.);
#3294=ORIENTED_EDGE('',*,*,#2260,.F.);
#3295=ORIENTED_EDGE('',*,*,#2263,.F.);
#3296=ORIENTED_EDGE('',*,*,#2266,.F.);
#3297=ORIENTED_EDGE('',*,*,#2269,.F.);
#3298=ORIENTED_EDGE('',*,*,#2272,.F.);
#3299=ORIENTED_EDGE('',*,*,#2329,.T.);
#3300=ORIENTED_EDGE('',*,*,#2331,.T.);
#3301=ORIENTED_EDGE('',*,*,#2343,.T.);
#3302=ORIENTED_EDGE('',*,*,#2339,.T.);
#3303=ORIENTED_EDGE('',*,*,#2336,.T.);
#3304=ORIENTED_EDGE('',*,*,#2352,.T.);
#3683=PLANE('',#4288);
#3684=PLANE('',#4292);
#3685=PLANE('',#4293);
#3686=PLANE('',#4297);
#3687=PLANE('',#4298);
#3688=PLANE('',#4301);
#3689=PLANE('',#4305);
#3690=PLANE('',#4308);
#3691=PLANE('',#4310);
#3692=PLANE('',#4311);
#3693=PLANE('',#4312);
#3694=PLANE('',#4313);
#3695=PLANE('',#4314);
#3696=PLANE('',#4318);
#3697=PLANE('',#4322);
#3698=PLANE('',#4323);
#3699=PLANE('',#4324);
#3700=PLANE('',#4325);
#3701=PLANE('',#4326);
#3702=PLANE('',#4334);
#3703=PLANE('',#4335);
#3704=PLANE('',#4336);
#3705=PLANE('',#4337);
#3706=PLANE('',#4338);
#3707=PLANE('',#4339);
#3708=PLANE('',#4340);
#3709=PLANE('',#4341);
#3710=PLANE('',#4342);
#3711=PLANE('',#4343);
#3859=ADVANCED_FACE('',(#618),#135,.F.);
#3860=ADVANCED_FACE('',(#619),#3683,.T.);
#3861=ADVANCED_FACE('',(#620),#136,.F.);
#3862=ADVANCED_FACE('',(#621),#3684,.T.);
#3863=ADVANCED_FACE('',(#622),#317,.T.);
#3864=ADVANCED_FACE('',(#623),#318,.T.);
#3865=ADVANCED_FACE('',(#624),#319,.T.);
#3866=ADVANCED_FACE('',(#625),#320,.T.);
#3867=ADVANCED_FACE('',(#626),#321,.T.);
#3868=ADVANCED_FACE('',(#627),#322,.T.);
#3869=ADVANCED_FACE('',(#628),#323,.T.);
#3870=ADVANCED_FACE('',(#629),#324,.T.);
#3871=ADVANCED_FACE('',(#630),#325,.T.);
#3872=ADVANCED_FACE('',(#631),#326,.T.);
#3873=ADVANCED_FACE('',(#632),#327,.T.);
#3874=ADVANCED_FACE('',(#633),#3685,.F.);
#3875=ADVANCED_FACE('',(#634),#137,.T.);
#3876=ADVANCED_FACE('',(#635),#3686,.F.);
#3877=ADVANCED_FACE('',(#636),#328,.T.);
#3878=ADVANCED_FACE('',(#637),#329,.T.);
#3879=ADVANCED_FACE('',(#638),#330,.T.);
#3880=ADVANCED_FACE('',(#639),#331,.T.);
#3881=ADVANCED_FACE('',(#640),#332,.T.);
#3882=ADVANCED_FACE('',(#641),#333,.T.);
#3883=ADVANCED_FACE('',(#642),#334,.T.);
#3884=ADVANCED_FACE('',(#643),#335,.T.);
#3885=ADVANCED_FACE('',(#644),#336,.T.);
#3886=ADVANCED_FACE('',(#645),#3687,.T.);
#3887=ADVANCED_FACE('',(#646),#138,.T.);
#3888=ADVANCED_FACE('',(#647),#3688,.T.);
#3889=ADVANCED_FACE('',(#648),#139,.F.);
#3890=ADVANCED_FACE('',(#649),#140,.T.);
#3891=ADVANCED_FACE('',(#650),#141,.F.);
#3892=ADVANCED_FACE('',(#651),#3689,.T.);
#3893=ADVANCED_FACE('',(#652),#142,.T.);
#3894=ADVANCED_FACE('',(#653),#3690,.T.);
#3895=ADVANCED_FACE('',(#654),#3691,.T.);
#3896=ADVANCED_FACE('',(#655),#3692,.T.);
#3897=ADVANCED_FACE('',(#656),#3693,.T.);
#3898=ADVANCED_FACE('',(#657),#3694,.T.);
#3899=ADVANCED_FACE('',(#658,#348,#349),#3695,.F.);
#3900=ADVANCED_FACE('',(#659),#143,.F.);
#3901=ADVANCED_FACE('',(#660),#3696,.F.);
#3902=ADVANCED_FACE('',(#661),#144,.T.);
#3903=ADVANCED_FACE('',(#662),#3697,.F.);
#3904=ADVANCED_FACE('',(#663),#3698,.T.);
#3905=ADVANCED_FACE('',(#664),#3699,.T.);
#3906=ADVANCED_FACE('',(#665),#3700,.T.);
#3907=ADVANCED_FACE('',(#666),#3701,.T.);
#3908=ADVANCED_FACE('',(#667),#101,.F.);
#3909=ADVANCED_FACE('',(#668),#145,.F.);
#3910=ADVANCED_FACE('',(#669),#146,.F.);
#3911=ADVANCED_FACE('',(#670),#3702,.F.);
#3912=ADVANCED_FACE('',(#671),#3703,.T.);
#3913=ADVANCED_FACE('',(#672),#3704,.T.);
#3914=ADVANCED_FACE('',(#673),#3705,.T.);
#3915=ADVANCED_FACE('',(#674),#3706,.T.);
#3916=ADVANCED_FACE('',(#675),#3707,.T.);
#3917=ADVANCED_FACE('',(#676),#3708,.T.);
#3918=ADVANCED_FACE('',(#677),#3709,.T.);
#3919=ADVANCED_FACE('',(#678,#350,#351),#3710,.T.);
#3920=ADVANCED_FACE('',(#679),#3711,.F.);
#4003=CLOSED_SHELL('',(#3859,#3860,#3861,#3862,#3863,#3864,#3865,#3866,
#3867,#3868,#3869,#3870,#3871,#3872,#3873,#3874,#3875,#3876,#3877,#3878,
#3879,#3880,#3881,#3882,#3883,#3884,#3885,#3886,#3887,#3888,#3889,#3890,
#3891,#3892,#3893,#3894,#3895,#3896,#3897,#3898,#3899,#3900,#3901,#3902,
#3903,#3904,#3905,#3906,#3907,#3908,#3909,#3910,#3911,#3912,#3913,#3914,
#3915,#3916,#3917,#3918,#3919,#3920));
#4284=AXIS2_PLACEMENT_3D('',#6712,#4969,#4970);
#4285=AXIS2_PLACEMENT_3D('',#6713,#4971,#4972);
#4286=AXIS2_PLACEMENT_3D('',#6715,#4973,#4974);
#4287=AXIS2_PLACEMENT_3D('',#6718,#4976,#4977);
#4288=AXIS2_PLACEMENT_3D('',#6719,#4978,#4979);
#4289=AXIS2_PLACEMENT_3D('',#6720,#4980,#4981);
#4290=AXIS2_PLACEMENT_3D('',#6722,#4982,#4983);
#4291=AXIS2_PLACEMENT_3D('',#6725,#4985,#4986);
#4292=AXIS2_PLACEMENT_3D('',#6726,#4987,#4988);
#4293=AXIS2_PLACEMENT_3D('',#7349,#4990,#4991);
#4294=AXIS2_PLACEMENT_3D('',#7353,#4994,#4995);
#4295=AXIS2_PLACEMENT_3D('',#7357,#4997,#4998);
#4296=AXIS2_PLACEMENT_3D('',#7360,#5000,#5001);
#4297=AXIS2_PLACEMENT_3D('',#7361,#5002,#5003);
#4298=AXIS2_PLACEMENT_3D('',#7879,#5005,#5006);
#4299=AXIS2_PLACEMENT_3D('',#7883,#5008,#5009);
#4300=AXIS2_PLACEMENT_3D('',#7886,#5012,#5013);
#4301=AXIS2_PLACEMENT_3D('',#7888,#5015,#5016);
#4302=AXIS2_PLACEMENT_3D('',#7890,#5018,#5019);
#4303=AXIS2_PLACEMENT_3D('',#7892,#5021,#5022);
#4304=AXIS2_PLACEMENT_3D('',#7894,#5024,#5025);
#4305=AXIS2_PLACEMENT_3D('',#7896,#5027,#5028);
#4306=AXIS2_PLACEMENT_3D('',#7898,#5030,#5031);
#4307=AXIS2_PLACEMENT_3D('',#7902,#5033,#5034);
#4308=AXIS2_PLACEMENT_3D('',#7904,#5036,#5037);
#4309=AXIS2_PLACEMENT_3D('',#7908,#5039,#5040);
#4310=AXIS2_PLACEMENT_3D('',#7910,#5042,#5043);
#4311=AXIS2_PLACEMENT_3D('',#7916,#5047,#5048);
#4312=AXIS2_PLACEMENT_3D('',#7920,#5051,#5052);
#4313=AXIS2_PLACEMENT_3D('',#7924,#5055,#5056);
#4314=AXIS2_PLACEMENT_3D('',#7926,#5058,#5059);
#4315=AXIS2_PLACEMENT_3D('',#7928,#5061,#5062);
#4316=AXIS2_PLACEMENT_3D('',#7930,#5063,#5064);
#4317=AXIS2_PLACEMENT_3D('',#7934,#5066,#5067);
#4318=AXIS2_PLACEMENT_3D('',#7936,#5069,#5070);
#4319=AXIS2_PLACEMENT_3D('',#7942,#5074,#5075);
#4320=AXIS2_PLACEMENT_3D('',#7944,#5076,#5077);
#4321=AXIS2_PLACEMENT_3D('',#7947,#5079,#5080);
#4322=AXIS2_PLACEMENT_3D('',#7948,#5081,#5082);
#4323=AXIS2_PLACEMENT_3D('',#7962,#5090,#5091);
#4324=AXIS2_PLACEMENT_3D('',#7966,#5094,#5095);
#4325=AXIS2_PLACEMENT_3D('',#7970,#5098,#5099);
#4326=AXIS2_PLACEMENT_3D('',#7974,#5102,#5103);
#4327=AXIS2_PLACEMENT_3D('',#7978,#5106,#5107);
#4328=AXIS2_PLACEMENT_3D('',#7980,#5108,#5109);
#4329=AXIS2_PLACEMENT_3D('',#7983,#5111,#5112);
#4330=AXIS2_PLACEMENT_3D('',#7985,#5113,#5114);
#4331=AXIS2_PLACEMENT_3D('',#7987,#5116,#5117);
#4332=AXIS2_PLACEMENT_3D('',#7989,#5118,#5119);
#4333=AXIS2_PLACEMENT_3D('',#7992,#5121,#5122);
#4334=AXIS2_PLACEMENT_3D('',#7993,#5123,#5124);
#4335=AXIS2_PLACEMENT_3D('',#7994,#5125,#5126);
#4336=AXIS2_PLACEMENT_3D('',#8003,#5131,#5132);
#4337=AXIS2_PLACEMENT_3D('',#8009,#5136,#5137);
#4338=AXIS2_PLACEMENT_3D('',#8018,#5143,#5144);
#4339=AXIS2_PLACEMENT_3D('',#8022,#5147,#5148);
#4340=AXIS2_PLACEMENT_3D('',#8026,#5151,#5152);
#4341=AXIS2_PLACEMENT_3D('',#8028,#5154,#5155);
#4342=AXIS2_PLACEMENT_3D('',#8031,#5158,#5159);
#4343=AXIS2_PLACEMENT_3D('',#8032,#5160,#5161);
#4969=DIRECTION('axis',(0.,0.,1.));
#4970=DIRECTION('refdir',(1.,0.,0.));
#4971=DIRECTION('center_axis',(1.,0.,0.));
#4972=DIRECTION('ref_axis',(0.,-1.,0.));
#4973=DIRECTION('center_axis',(1.,0.,0.));
#4974=DIRECTION('ref_axis',(0.,-1.,0.));
#4975=DIRECTION('',(1.,0.,0.));
#4976=DIRECTION('center_axis',(1.,0.,0.));
#4977=DIRECTION('ref_axis',(0.,-1.,0.));
#4978=DIRECTION('center_axis',(-1.,0.,0.));
#4979=DIRECTION('ref_axis',(0.,-1.,0.));
#4980=DIRECTION('center_axis',(1.,0.,0.));
#4981=DIRECTION('ref_axis',(0.,-1.,0.));
#4982=DIRECTION('center_axis',(1.,0.,0.));
#4983=DIRECTION('ref_axis',(0.,-1.,0.));
#4984=DIRECTION('',(1.,0.,0.));
#4985=DIRECTION('center_axis',(1.,0.,0.));
#4986=DIRECTION('ref_axis',(0.,-1.,0.));
#4987=DIRECTION('center_axis',(-1.,0.,0.));
#4988=DIRECTION('ref_axis',(0.,-1.,0.));
#4989=DIRECTION('',(-1.,0.,0.));
#4990=DIRECTION('center_axis',(-1.,0.,0.));
#4991=DIRECTION('ref_axis',(0.,-1.,0.));
#4992=DIRECTION('',(0.,1.,-2.53765262771464E-16));
#4993=DIRECTION('',(0.,2.02447305031589E-16,-1.));
#4994=DIRECTION('center_axis',(0.,-1.,2.53765262771464E-16));
#4995=DIRECTION('ref_axis',(0.707106781186548,1.79439138135289E-16,0.707106781186548));
#4996=DIRECTION('',(0.,1.,-2.53765262771464E-16));
#4997=DIRECTION('center_axis',(0.,-0.999999999997375,-2.2912420403343E-6));
#4998=DIRECTION('ref_axis',(0.,-2.2912420403343E-6,0.999999999997375));
#4999=DIRECTION('',(0.,-1.,2.53765262771464E-16));
#5000=DIRECTION('center_axis',(0.,1.,2.02447305031589E-16));
#5001=DIRECTION('ref_axis',(0.707106781186548,1.79439138135289E-16,0.707106781186548));
#5002=DIRECTION('center_axis',(-1.,0.,0.));
#5003=DIRECTION('ref_axis',(0.,-1.,0.));
#5004=DIRECTION('',(0.,-2.2912420403343E-6,0.999999999997375));
#5005=DIRECTION('center_axis',(0.,-1.,0.));
#5006=DIRECTION('ref_axis',(0.,0.,1.));
#5007=DIRECTION('',(-1.,0.,0.));
#5008=DIRECTION('center_axis',(0.,1.,0.));
#5009=DIRECTION('ref_axis',(5.92118946466749E-15,0.,-1.));
#5010=DIRECTION('',(-1.,0.,0.));
#5011=DIRECTION('',(-1.,0.,0.));
#5012=DIRECTION('center_axis',(-1.,0.,0.));
#5013=DIRECTION('ref_axis',(0.,5.15150041143406E-8,0.999999999999999));
#5014=DIRECTION('',(-1.,0.,0.));
#5015=DIRECTION('center_axis',(0.,5.15150011224698E-8,0.999999999999999));
#5016=DIRECTION('ref_axis',(0.,0.999999999999999,-5.15150011224698E-8));
#5017=DIRECTION('',(-1.,0.,0.));
#5018=DIRECTION('center_axis',(-1.,0.,0.));
#5019=DIRECTION('ref_axis',(0.,-9.9257750216751E-16,-1.));
#5020=DIRECTION('',(-1.,0.,0.));
#5021=DIRECTION('center_axis',(-1.,0.,0.));
#5022=DIRECTION('ref_axis',(0.,0.981911225094666,0.189341876068374));
#5023=DIRECTION('',(-1.,0.,0.));
#5024=DIRECTION('center_axis',(-1.,0.,0.));
#5025=DIRECTION('ref_axis',(0.,-0.981911225094667,-0.18934187606837));
#5026=DIRECTION('',(-1.,0.,0.));
#5027=DIRECTION('center_axis',(0.,-5.15150011224698E-8,0.999999999999999));
#5028=DIRECTION('ref_axis',(0.,0.999999999999999,5.15150011224698E-8));
#5029=DIRECTION('',(-1.,0.,0.));
#5030=DIRECTION('center_axis',(-1.,0.,0.));
#5031=DIRECTION('ref_axis',(0.,1.,-2.96059473233376E-15));
#5032=DIRECTION('',(-1.,0.,0.));
#5033=DIRECTION('center_axis',(1.,0.,0.));
#5034=DIRECTION('ref_axis',(0.,1.,-2.96059473233376E-15));
#5035=DIRECTION('',(1.,0.,0.));
#5036=DIRECTION('center_axis',(0.,1.,0.));
#5037=DIRECTION('ref_axis',(0.,0.,-1.));
#5038=DIRECTION('',(-1.,0.,0.));
#5039=DIRECTION('center_axis',(0.,-1.,0.));
#5040=DIRECTION('ref_axis',(5.92118946466749E-15,0.,-1.));
#5041=DIRECTION('',(0.,0.,1.));
#5042=DIRECTION('center_axis',(0.,0.,-1.));
#5043=DIRECTION('ref_axis',(0.,-1.,0.));
#5044=DIRECTION('',(0.,1.,0.));
#5045=DIRECTION('',(-1.,0.,0.));
#5046=DIRECTION('',(0.,1.,0.));
#5047=DIRECTION('center_axis',(0.,-1.,-2.02447305031589E-16));
#5048=DIRECTION('ref_axis',(0.,2.02447305031589E-16,-1.));
#5049=DIRECTION('',(1.,0.,0.));
#5050=DIRECTION('',(0.,2.02447305031589E-16,-1.));
#5051=DIRECTION('center_axis',(0.,2.53765262771464E-16,1.));
#5052=DIRECTION('ref_axis',(0.,-1.,2.53765262771464E-16));
#5053=DIRECTION('',(1.,0.,0.));
#5054=DIRECTION('',(0.,1.,-2.53765262771464E-16));
#5055=DIRECTION('center_axis',(0.,0.999999999997375,2.2912420403343E-6));
#5056=DIRECTION('ref_axis',(0.,-2.2912420403343E-6,0.999999999997375));
#5057=DIRECTION('',(0.,2.2912420403343E-6,-0.999999999997375));
#5058=DIRECTION('center_axis',(1.,0.,0.));
#5059=DIRECTION('ref_axis',(0.,0.,1.));
#5060=DIRECTION('',(0.,-1.,0.));
#5061=DIRECTION('center_axis',(0.,-1.,0.));
#5062=DIRECTION('ref_axis',(5.92118946466749E-15,0.,-1.));
#5063=DIRECTION('center_axis',(0.,-1.,0.));
#5064=DIRECTION('ref_axis',(5.92118946466749E-15,0.,-1.));
#5065=DIRECTION('',(0.,-1.,0.));
#5066=DIRECTION('center_axis',(0.,1.,0.));
#5067=DIRECTION('ref_axis',(5.92118946466749E-15,0.,-1.));
#5068=DIRECTION('',(0.,1.,0.));
#5069=DIRECTION('center_axis',(-3.9666966593473E-16,0.,-1.));
#5070=DIRECTION('ref_axis',(1.,0.,-3.9666966593473E-16));
#5071=DIRECTION('',(1.,0.,-3.9666966593473E-16));
#5072=DIRECTION('',(0.,-1.,0.));
#5073=DIRECTION('',(-1.,0.,3.9666966593473E-16));
#5074=DIRECTION('center_axis',(0.,-1.,0.));
#5075=DIRECTION('ref_axis',(2.96059473233377E-15,0.,1.));
#5076=DIRECTION('center_axis',(0.,1.,0.));
#5077=DIRECTION('ref_axis',(2.96059473233377E-15,0.,1.));
#5078=DIRECTION('',(0.,-1.,0.));
#5079=DIRECTION('center_axis',(0.,-1.,0.));
#5080=DIRECTION('ref_axis',(2.96059473233377E-15,0.,1.));
#5081=DIRECTION('center_axis',(0.965925826289068,0.,-0.258819045102521));
#5082=DIRECTION('ref_axis',(0.258819045102521,0.,0.965925826289068));
#5083=DIRECTION('',(0.258819045102521,0.,0.965925826289068));
#5084=DIRECTION('',(0.,1.,0.));
#5085=DIRECTION('',(0.258819045102521,0.,0.965925826289068));
#5086=DIRECTION('',(0.,-1.,0.));
#5087=DIRECTION('',(-0.258819045102521,0.,-0.965925826289068));
#5088=DIRECTION('',(0.,1.,0.));
#5089=DIRECTION('',(-0.258819045102521,0.,-0.965925826289068));
#5090=DIRECTION('center_axis',(0.,0.,-1.));
#5091=DIRECTION('ref_axis',(0.,-1.,0.));
#5092=DIRECTION('',(-1.,0.,0.));
#5093=DIRECTION('',(0.,-1.,0.));
#5094=DIRECTION('center_axis',(0.,-1.,0.));
#5095=DIRECTION('ref_axis',(0.,0.,1.));
#5096=DIRECTION('',(-1.,0.,0.));
#5097=DIRECTION('',(0.,0.,1.));
#5098=DIRECTION('center_axis',(0.,0.,-1.));
#5099=DIRECTION('ref_axis',(0.,-1.,0.));
#5100=DIRECTION('',(-1.,0.,0.));
#5101=DIRECTION('',(0.,-1.,0.));
#5102=DIRECTION('center_axis',(0.,-1.,0.));
#5103=DIRECTION('ref_axis',(0.,0.,1.));
#5104=DIRECTION('',(-1.,0.,0.));
#5105=DIRECTION('',(0.,0.,1.));
#5106=DIRECTION('center_axis',(1.,0.,0.));
#5107=DIRECTION('ref_axis',(0.,1.,0.));
#5108=DIRECTION('center_axis',(-1.,0.,0.));
#5109=DIRECTION('ref_axis',(0.,1.,0.));
#5110=DIRECTION('',(-0.642787609686539,0.766044443118978,-9.38133875270273E-17));
#5111=DIRECTION('center_axis',(-1.,0.,0.));
#5112=DIRECTION('ref_axis',(0.,1.,0.));
#5113=DIRECTION('center_axis',(-1.,0.,0.));
#5114=DIRECTION('ref_axis',(0.,1.,0.));
#5115=DIRECTION('',(-1.,0.,0.));
#5116=DIRECTION('center_axis',(-1.,0.,0.));
#5117=DIRECTION('ref_axis',(0.,1.,0.));
#5118=DIRECTION('center_axis',(-1.,0.,0.));
#5119=DIRECTION('ref_axis',(0.,1.,0.));
#5120=DIRECTION('',(-1.,0.,0.));
#5121=DIRECTION('center_axis',(-1.,0.,0.));
#5122=DIRECTION('ref_axis',(0.,1.,0.));
#5123=DIRECTION('center_axis',(-1.,0.,0.));
#5124=DIRECTION('ref_axis',(0.,1.,0.));
#5125=DIRECTION('center_axis',(0.,0.,-1.));
#5126=DIRECTION('ref_axis',(0.,-1.,0.));
#5127=DIRECTION('',(0.,1.,0.));
#5128=DIRECTION('',(-1.,0.,0.));
#5129=DIRECTION('',(0.,-1.,0.));
#5130=DIRECTION('',(-1.,0.,0.));
#5131=DIRECTION('center_axis',(0.,1.,0.));
#5132=DIRECTION('ref_axis',(0.,0.,-1.));
#5133=DIRECTION('',(0.,0.,1.));
#5134=DIRECTION('',(0.,0.,-1.));
#5135=DIRECTION('',(-1.,0.,0.));
#5136=DIRECTION('center_axis',(0.,0.,1.));
#5137=DIRECTION('ref_axis',(0.,1.,0.));
#5138=DIRECTION('',(-1.,0.,0.));
#5139=DIRECTION('',(0.,-1.,0.));
#5140=DIRECTION('',(0.,1.,0.));
#5141=DIRECTION('',(-1.,0.,0.));
#5142=DIRECTION('',(0.,1.,0.));
#5143=DIRECTION('center_axis',(0.,1.,0.));
#5144=DIRECTION('ref_axis',(0.,0.,-1.));
#5145=DIRECTION('',(-1.,0.,0.));
#5146=DIRECTION('',(0.,0.,1.));
#5147=DIRECTION('center_axis',(0.,0.,-1.));
#5148=DIRECTION('ref_axis',(0.,-1.,0.));
#5149=DIRECTION('',(-1.,0.,0.));
#5150=DIRECTION('',(0.,1.,0.));
#5151=DIRECTION('center_axis',(0.,1.,0.));
#5152=DIRECTION('ref_axis',(0.,0.,-1.));
#5153=DIRECTION('',(0.,0.,1.));
#5154=DIRECTION('center_axis',(0.,-1.,0.));
#5155=DIRECTION('ref_axis',(0.,0.,1.));
#5156=DIRECTION('',(0.,0.,1.));
#5157=DIRECTION('',(0.,0.,1.));
#5158=DIRECTION('center_axis',(1.,0.,0.));
#5159=DIRECTION('ref_axis',(0.,1.,0.));
#5160=DIRECTION('center_axis',(1.,0.,0.));
#5161=DIRECTION('ref_axis',(0.,1.,0.));
#6712=CARTESIAN_POINT('',(0.,0.,0.));
#6713=CARTESIAN_POINT('Origin',(-40.,19.,55.));
#6714=CARTESIAN_POINT('',(-40.,22.,55.));
#6715=CARTESIAN_POINT('Origin',(-40.,19.,55.));
#6716=CARTESIAN_POINT('',(-22.,22.,55.));
#6717=CARTESIAN_POINT('',(-40.,22.,55.));
#6718=CARTESIAN_POINT('Origin',(-22.,19.,55.));
#6719=CARTESIAN_POINT('Origin',(-22.,19.,55.));
#6720=CARTESIAN_POINT('Origin',(-40.,-19.0000002831221,55.));
#6721=CARTESIAN_POINT('',(-40.,-16.0000002831221,55.));
#6722=CARTESIAN_POINT('Origin',(-40.,-19.0000002831221,55.));
#6723=CARTESIAN_POINT('',(-22.,-16.0000002831221,55.));
#6724=CARTESIAN_POINT('',(-40.,-16.0000002831221,55.));
#6725=CARTESIAN_POINT('Origin',(-22.,-19.0000002831221,55.));
#6726=CARTESIAN_POINT('Origin',(-22.,-19.0000002831221,55.));
#6727=CARTESIAN_POINT('Ctrl Pts',(-6.37867965644035,34.9999541371497,51.0165890496372));
#6728=CARTESIAN_POINT('Ctrl Pts',(-6.37867965644035,34.9950012836112,51.9122953199069));
#6729=CARTESIAN_POINT('Ctrl Pts',(-6.37867965644035,34.2384990747876,53.4551378138109));
#6730=CARTESIAN_POINT('Ctrl Pts',(-6.37867965644035,32.6710924757466,54.000000684689));
#6731=CARTESIAN_POINT('Ctrl Pts',(-6.37867965644035,31.999999845455,54.0000006501177));
#6732=CARTESIAN_POINT('Ctrl Pts',(-6.66439394215464,34.9999541371497,51.0165890496372));
#6733=CARTESIAN_POINT('Ctrl Pts',(-6.66439394215464,34.9950007331352,51.9123948715632));
#6734=CARTESIAN_POINT('Ctrl Pts',(-6.66439394215464,34.2386138683966,53.4551824004139));
#6735=CARTESIAN_POINT('Ctrl Pts',(-6.66439394215464,32.6711670631254,54.0000006846929));
#6736=CARTESIAN_POINT('Ctrl Pts',(-6.66439394215464,31.999999845455,54.0000006501177));
#6737=CARTESIAN_POINT('Ctrl Pts',(-7.29086286479755,35.1192315079769,51.0172485999472));
#6738=CARTESIAN_POINT('Ctrl Pts',(-7.29086286479755,35.1140827400347,51.9483853061338));
#6739=CARTESIAN_POINT('Ctrl Pts',(-7.29086286479755,34.3272906341022,53.5526716241217));
#6740=CARTESIAN_POINT('Ctrl Pts',(-7.29086286479755,32.6976381187965,54.1192798803784));
#6741=CARTESIAN_POINT('Ctrl Pts',(-7.29086286479755,31.9999998393103,54.1192798444396));
#6742=CARTESIAN_POINT('Ctrl Pts',(-8.04466290756678,35.7074899498764,51.0205014050265));
#6743=CARTESIAN_POINT('Ctrl Pts',(-8.04466290756678,35.7013690886002,52.1274377967375));
#6744=CARTESIAN_POINT('Ctrl Pts',(-8.04466290756678,34.7664221252725,54.0341696623003));
#6745=CARTESIAN_POINT('Ctrl Pts',(-8.04466290756678,32.8293530013812,54.7075473222703));
#6746=CARTESIAN_POINT('Ctrl Pts',(-8.04466290756678,31.9999998090057,54.7075472795461));
#6747=CARTESIAN_POINT('Ctrl Pts',(-8.43400626930132,36.4500762616906,51.0246075739394));
#6748=CARTESIAN_POINT('Ctrl Pts',(-8.43400626930132,36.4427288681681,52.3533580401398));
#6749=CARTESIAN_POINT('Ctrl Pts',(-8.43400626930133,35.3206360783581,54.6419397551437));
#6750=CARTESIAN_POINT('Ctrl Pts',(-8.43400626930132,32.9955433713278,55.4501449951943));
#6751=CARTESIAN_POINT('Ctrl Pts',(-8.43400626930132,31.9999997707508,55.4501449439089));
#6752=CARTESIAN_POINT('Ctrl Pts',(-8.5,36.906959612409,51.0271339337466));
#6753=CARTESIAN_POINT('Ctrl Pts',(-8.5,36.8988586235225,52.4921694904538));
#6754=CARTESIAN_POINT('Ctrl Pts',(-8.5,35.6614045759983,55.0157918682276));
#6755=CARTESIAN_POINT('Ctrl Pts',(-8.5,33.0976526250101,55.9070353359372));
#6756=CARTESIAN_POINT('Ctrl Pts',(-8.5,31.9999997472141,55.9070352793916));
#6757=CARTESIAN_POINT('Ctrl Pts',(-8.5,37.1212420507768,51.0283188194265));
#6758=CARTESIAN_POINT('Ctrl Pts',(-8.5,37.1127870009151,52.5573850673551));
#6759=CARTESIAN_POINT('Ctrl Pts',(-8.5,35.8213569502497,55.1911819510015));
#6760=CARTESIAN_POINT('Ctrl Pts',(-8.5,33.1456265161503,56.1213210526943));
#6761=CARTESIAN_POINT('Ctrl Pts',(-8.5,31.9999997361752,56.1213209936773));
#6762=CARTESIAN_POINT('',(-8.5,31.9999997361752,56.1213209936773));
#6763=CARTESIAN_POINT('',(-6.37867965644035,31.999999845455,54.0000006501177));
#6764=CARTESIAN_POINT('Ctrl Pts',(-8.5,31.9999997361752,56.1213209936773));
#6765=CARTESIAN_POINT('Ctrl Pts',(-8.5,31.9999997472141,55.9070352793916));
#6766=CARTESIAN_POINT('Ctrl Pts',(-8.43400626930132,31.9999997707508,55.4501449439089));
#6767=CARTESIAN_POINT('Ctrl Pts',(-8.04466290756678,31.9999998090057,54.7075472795461));
#6768=CARTESIAN_POINT('Ctrl Pts',(-7.29086286479755,31.9999998393103,54.1192798444396));
#6769=CARTESIAN_POINT('Ctrl Pts',(-6.66439394215464,31.999999845455,54.0000006501177));
#6770=CARTESIAN_POINT('Ctrl Pts',(-6.37867965644035,31.999999845455,54.0000006501177));
#6771=CARTESIAN_POINT('',(-6.37867965644035,34.9999541371497,51.0165890496372));
#6772=CARTESIAN_POINT('Ctrl Pts',(-6.37867965644035,31.999999845455,54.0000006501177));
#6773=CARTESIAN_POINT('Ctrl Pts',(-6.37867965644035,32.6710924757466,54.000000684689));
#6774=CARTESIAN_POINT('Ctrl Pts',(-6.37867965644035,34.2384990747876,53.4551378138109));
#6775=CARTESIAN_POINT('Ctrl Pts',(-6.37867965644035,34.9950012836112,51.9122953199069));
#6776=CARTESIAN_POINT('Ctrl Pts',(-6.37867965644035,34.9999541371497,51.0165890496372));
#6777=CARTESIAN_POINT('',(-8.5,34.9999446647671,55.1506938537381));
#6778=CARTESIAN_POINT('Ctrl Pts',(-6.37867965644035,34.9999541371497,51.0165890496373));
#6779=CARTESIAN_POINT('Ctrl Pts',(-6.38025523414058,34.9999541371497,51.0165890496373));
#6780=CARTESIAN_POINT('Ctrl Pts',(-6.38176387508139,34.9999541364188,51.0169080380021));
#6781=CARTESIAN_POINT('Ctrl Pts',(-6.3850668587029,34.9999541336229,51.0181283084381));
#6782=CARTESIAN_POINT('Ctrl Pts',(-6.38702023223131,34.9999541311292,51.0192166501386));
#6783=CARTESIAN_POINT('Ctrl Pts',(-6.39241151026715,34.9999541222732,51.0230818054667));
#6784=CARTESIAN_POINT('Ctrl Pts',(-6.39586971593905,34.9999541150669,51.0262269686459));
#6785=CARTESIAN_POINT('Ctrl Pts',(-6.4053209430701,34.9999540937118,51.0355472789196));
#6786=CARTESIAN_POINT('Ctrl Pts',(-6.4125881509423,34.9999540754092,51.0435353194066));
#6787=CARTESIAN_POINT('Ctrl Pts',(-6.43129945172038,34.9999540271935,51.0645787901438));
#6788=CARTESIAN_POINT('Ctrl Pts',(-6.44799684949083,34.9999539825086,51.0840813028394));
#6789=CARTESIAN_POINT('Ctrl Pts',(-6.48257634326567,34.9999538896126,51.1246252399336));
#6790=CARTESIAN_POINT('Ctrl Pts',(-6.51348072849312,34.9999538056414,51.161273784187));
#6791=CARTESIAN_POINT('Ctrl Pts',(-6.58721417125074,34.9999536047906,51.2489339939019));
#6792=CARTESIAN_POINT('Ctrl Pts',(-6.64388575517693,34.9999534494532,51.3167302659389));
#6793=CARTESIAN_POINT('Ctrl Pts',(-6.8042901846373,34.9999530064479,51.5100775053381));
#6794=CARTESIAN_POINT('Ctrl Pts',(-6.91298478299303,34.9999527015254,51.6431593731394));
#6795=CARTESIAN_POINT('Ctrl Pts',(-7.23837215274935,34.9999517601401,52.0540217934736));
#6796=CARTESIAN_POINT('Ctrl Pts',(-7.4499833285231,34.9999511070469,52.3390607643293));
#6797=CARTESIAN_POINT('Ctrl Pts',(-7.96154279702925,34.9999492924801,53.1310184777057));
#6798=CARTESIAN_POINT('Ctrl Pts',(-8.30443682747778,34.9999478076447,53.7790667327638));
#6799=CARTESIAN_POINT('Ctrl Pts',(-8.47893057631952,34.9999456402076,54.7250327436578));
#6800=CARTESIAN_POINT('Ctrl Pts',(-8.5,34.9999451531404,54.9376105145217));
#6801=CARTESIAN_POINT('Ctrl Pts',(-8.5,34.9999446649149,55.1506938535244));
#6802=CARTESIAN_POINT('Ctrl Pts',(-8.5,35.0003235118796,55.1512179007789));
#6803=CARTESIAN_POINT('Ctrl Pts',(-8.5,34.1372307533344,55.7747966654739));
#6804=CARTESIAN_POINT('Ctrl Pts',(-8.5,33.0681306896806,56.1213210487021));
#6805=CARTESIAN_POINT('Ctrl Pts',(-8.5,31.9999997361752,56.1213209936773));
#6806=CARTESIAN_POINT('Ctrl Pts',(-6.37867965644035,31.999999845455,54.0000006501177));
#6807=CARTESIAN_POINT('Ctrl Pts',(-6.37867965644035,27.7891836451619,54.0000004331975));
#6808=CARTESIAN_POINT('Ctrl Pts',(-6.37867965644035,23.5940884943755,54.0000002170871));
#6809=CARTESIAN_POINT('Ctrl Pts',(-6.37867965644035,19.3800314873921,54.));
#6810=CARTESIAN_POINT('Ctrl Pts',(-6.66439394215464,31.999999845455,54.0000006501177));
#6811=CARTESIAN_POINT('Ctrl Pts',(-6.66439394215464,27.7891836451619,54.0000004331975));
#6812=CARTESIAN_POINT('Ctrl Pts',(-6.66439394215464,23.5940884943755,54.0000002170871));
#6813=CARTESIAN_POINT('Ctrl Pts',(-6.66439394215464,19.3800314873921,54.));
#6814=CARTESIAN_POINT('Ctrl Pts',(-7.29086126549403,31.9999998393104,54.1192791631438));
#6815=CARTESIAN_POINT('Ctrl Pts',(-7.29086126549403,27.7891836390173,54.1192789462237));
#6816=CARTESIAN_POINT('Ctrl Pts',(-7.29086126549403,23.5940884882309,54.1192787301133));
#6817=CARTESIAN_POINT('Ctrl Pts',(-7.29086126549403,19.3800314812474,54.1192785130262));
#6818=CARTESIAN_POINT('Ctrl Pts',(-8.04466232388412,31.9999998090057,54.7075471088815));
#6819=CARTESIAN_POINT('Ctrl Pts',(-8.04466232388412,27.7891836087127,54.7075468919613));
#6820=CARTESIAN_POINT('Ctrl Pts',(-8.04466232388412,23.5940884579263,54.707546675851));
#6821=CARTESIAN_POINT('Ctrl Pts',(-8.04466232388412,19.3800314509428,54.7075464587638));
#6822=CARTESIAN_POINT('Ctrl Pts',(-8.43400552734115,31.9999997707508,55.4501449226738));
#6823=CARTESIAN_POINT('Ctrl Pts',(-8.43400552734115,27.7891835704577,55.4501447057536));
#6824=CARTESIAN_POINT('Ctrl Pts',(-8.43400552734115,23.5940884196713,55.4501444896432));
#6825=CARTESIAN_POINT('Ctrl Pts',(-8.43400552734115,19.3800314126879,55.4501442725561));
#6826=CARTESIAN_POINT('Ctrl Pts',(-8.5,31.9999997472141,55.9070352793916));
#6827=CARTESIAN_POINT('Ctrl Pts',(-8.5,27.789183546921,55.9070350624714));
#6828=CARTESIAN_POINT('Ctrl Pts',(-8.5,23.5940883961346,55.9070348463611));
#6829=CARTESIAN_POINT('Ctrl Pts',(-8.5,19.3800313891512,55.9070346292739));
#6830=CARTESIAN_POINT('Ctrl Pts',(-8.5,31.9999997361752,56.1213209936773));
#6831=CARTESIAN_POINT('Ctrl Pts',(-8.5,27.7891835358821,56.1213207767571));
#6832=CARTESIAN_POINT('Ctrl Pts',(-8.5,23.5940883850957,56.1213205606468));
#6833=CARTESIAN_POINT('Ctrl Pts',(-8.5,19.3800313781122,56.1213203435596));
#6834=CARTESIAN_POINT('',(-8.5,19.3800313781122,56.1213203435596));
#6835=CARTESIAN_POINT('',(-6.37867965644035,19.3800314873921,54.));
#6836=CARTESIAN_POINT('Ctrl Pts',(-8.5,19.3800313781122,56.1213203435596));
#6837=CARTESIAN_POINT('Ctrl Pts',(-8.5,19.3800313891512,55.9070346292739));
#6838=CARTESIAN_POINT('Ctrl Pts',(-8.43400552734115,19.3800314126879,55.4501442725561));
#6839=CARTESIAN_POINT('Ctrl Pts',(-8.04466232388412,19.3800314509428,54.7075464587638));
#6840=CARTESIAN_POINT('Ctrl Pts',(-7.29086126549403,19.3800314812474,54.1192785130262));
#6841=CARTESIAN_POINT('Ctrl Pts',(-6.66439394215464,19.3800314873921,54.));
#6842=CARTESIAN_POINT('Ctrl Pts',(-6.37867965644035,19.3800314873921,54.));
#6843=CARTESIAN_POINT('Ctrl Pts',(-6.37867965644035,19.3800314873921,54.));
#6844=CARTESIAN_POINT('Ctrl Pts',(-6.37867965644035,23.5940884943755,54.0000002170871));
#6845=CARTESIAN_POINT('Ctrl Pts',(-6.37867965644035,27.7891836451619,54.0000004331975));
#6846=CARTESIAN_POINT('Ctrl Pts',(-6.37867965644035,31.999999845455,54.0000006501177));
#6847=CARTESIAN_POINT('Ctrl Pts',(-8.5,31.9999997361752,56.1213209936773));
#6848=CARTESIAN_POINT('Ctrl Pts',(-8.5,27.7891835358821,56.1213207767571));
#6849=CARTESIAN_POINT('Ctrl Pts',(-8.5,23.5940883850957,56.1213205606468));
#6850=CARTESIAN_POINT('Ctrl Pts',(-8.5,19.3800313781122,56.1213203435596));
#6851=CARTESIAN_POINT('Ctrl Pts',(-6.37867965644035,19.3800304312095,54.0000000000003));
#6852=CARTESIAN_POINT('Ctrl Pts',(-6.37867965644035,18.9297963927261,54.00000021257));
#6853=CARTESIAN_POINT('Ctrl Pts',(-6.37867965644035,17.9034130389181,54.3199295949321));
#6854=CARTESIAN_POINT('Ctrl Pts',(-6.37867965644035,17.2949884311804,55.2350357080536));
#6855=CARTESIAN_POINT('Ctrl Pts',(-6.37867965644035,17.1834464391566,55.8134832037259));
#6856=CARTESIAN_POINT('Ctrl Pts',(-6.66439394215464,19.3800304312095,54.0000000000003));
#6857=CARTESIAN_POINT('Ctrl Pts',(-6.66439394215464,18.9298634995458,54.0000002125383));
#6858=CARTESIAN_POINT('Ctrl Pts',(-6.66439394215464,17.9035184186743,54.3199764064705));
#6859=CARTESIAN_POINT('Ctrl Pts',(-6.66439394215464,17.2949718059861,55.2351219249287));
#6860=CARTESIAN_POINT('Ctrl Pts',(-6.66439394215464,17.1834464391566,55.8134832037259));
#6861=CARTESIAN_POINT('Ctrl Pts',(-7.29085029793421,19.3800304875225,54.1192738233668));
#6862=CARTESIAN_POINT('Ctrl Pts',(-7.29085029793421,18.9536797671411,54.1192740246605));
#6863=CARTESIAN_POINT('Ctrl Pts',(-7.29085029793421,17.9819509665207,54.4220604781489));
#6864=CARTESIAN_POINT('Ctrl Pts',(-7.29085029793421,17.4061878303299,55.2883038245807));
#6865=CARTESIAN_POINT('Ctrl Pts',(-7.29085029793421,17.3005627451802,55.8360667332079));
#6866=CARTESIAN_POINT('Ctrl Pts',(-8.04465837989031,19.3800307652641,54.7075453005511));
#6867=CARTESIAN_POINT('Ctrl Pts',(-8.04465837989031,19.0721849320778,54.7075454458949));
#6868=CARTESIAN_POINT('Ctrl Pts',(-8.04465837989031,18.3704231339243,54.9262762166006));
#6869=CARTESIAN_POINT('Ctrl Pts',(-8.04465837989031,17.9544595302371,55.5519398552372));
#6870=CARTESIAN_POINT('Ctrl Pts',(-8.04465837989031,17.8781931120305,55.9474511583354));
#6871=CARTESIAN_POINT('Ctrl Pts',(-8.43400047932409,19.3800311158686,55.4501441545312));
#6872=CARTESIAN_POINT('Ctrl Pts',(-8.43400047932409,19.221708029536,55.4501442292806));
#6873=CARTESIAN_POINT('Ctrl Pts',(-8.43400047932409,18.8606961296434,55.5627187553402));
#6874=CARTESIAN_POINT('Ctrl Pts',(-8.43400047932409,18.6465825795345,55.8846473578588));
#6875=CARTESIAN_POINT('Ctrl Pts',(-8.43400047932409,18.6073592624962,56.0880562185142));
#6876=CARTESIAN_POINT('Ctrl Pts',(-8.5,19.3800313315811,55.907034629274));
#6877=CARTESIAN_POINT('Ctrl Pts',(-8.5,19.3135767217403,55.9070346606493));
#6878=CARTESIAN_POINT('Ctrl Pts',(-8.5,19.1621419276791,55.9542072360834));
#6879=CARTESIAN_POINT('Ctrl Pts',(-8.5,19.0724487625994,56.0891857833112));
#6880=CARTESIAN_POINT('Ctrl Pts',(-8.5,19.055985148285,56.1745647181597));
#6881=CARTESIAN_POINT('Ctrl Pts',(-8.5,19.3800314327522,56.1213203435597));
#6882=CARTESIAN_POINT('Ctrl Pts',(-8.5,19.3567392996677,56.1213203545566));
#6883=CARTESIAN_POINT('Ctrl Pts',(-8.5,19.3036410093805,56.1378713860528));
#6884=CARTESIAN_POINT('Ctrl Pts',(-8.5,19.2721651418894,56.1852129274543));
#6885=CARTESIAN_POINT('Ctrl Pts',(-8.5,19.2663946965196,56.2151379773172));
#6886=CARTESIAN_POINT('',(-8.5,19.2663946965196,56.2151379773172));
#6887=CARTESIAN_POINT('',(-6.37867965644035,17.1834464391566,55.8134832037257));
#6888=CARTESIAN_POINT('Ctrl Pts',(-8.5,19.2663946965196,56.2151379773172));
#6889=CARTESIAN_POINT('Ctrl Pts',(-8.5,19.055985148285,56.1745647181597));
#6890=CARTESIAN_POINT('Ctrl Pts',(-8.43400047932409,18.6073592624962,56.0880562185142));
#6891=CARTESIAN_POINT('Ctrl Pts',(-8.04465837989031,17.8781931120305,55.9474511583354));
#6892=CARTESIAN_POINT('Ctrl Pts',(-7.29085029793421,17.3005627451802,55.8360667332079));
#6893=CARTESIAN_POINT('Ctrl Pts',(-6.66439394215464,17.1834464391566,55.8134832037259));
#6894=CARTESIAN_POINT('Ctrl Pts',(-6.37867965644035,17.1834464391566,55.8134832037259));
#6895=CARTESIAN_POINT('Ctrl Pts',(-6.37867965644035,17.1834464391566,55.8134832037259));
#6896=CARTESIAN_POINT('Ctrl Pts',(-6.37867965644035,17.2949884311804,55.2350357080536));
#6897=CARTESIAN_POINT('Ctrl Pts',(-6.37867965644035,17.9034130389181,54.3199295949321));
#6898=CARTESIAN_POINT('Ctrl Pts',(-6.37867965644035,18.9297963927261,54.00000021257));
#6899=CARTESIAN_POINT('Ctrl Pts',(-6.37867965644035,19.3800304312095,54.0000000000003));
#6900=CARTESIAN_POINT('Ctrl Pts',(-8.5,19.3800313781122,56.1213203435597));
#6901=CARTESIAN_POINT('Ctrl Pts',(-8.5,19.3567392640789,56.1213203656498));
#6902=CARTESIAN_POINT('Ctrl Pts',(-8.5,19.3036409988323,56.137871401918));
#6903=CARTESIAN_POINT('Ctrl Pts',(-8.5,19.2721651418894,56.1852129274543));
#6904=CARTESIAN_POINT('Ctrl Pts',(-8.5,19.2663946965196,56.2151379773172));
#6905=CARTESIAN_POINT('Ctrl Pts',(-6.37867965644035,17.1834464391567,55.8134832037256));
#6906=CARTESIAN_POINT('Ctrl Pts',(-6.37867965644035,17.1179077550972,56.1533613695715));
#6907=CARTESIAN_POINT('Ctrl Pts',(-6.37867965644035,17.0393555263014,56.5042886864595));
#6908=CARTESIAN_POINT('Ctrl Pts',(-6.37867965644035,16.9519317108386,56.8453440034822));
#6909=CARTESIAN_POINT('Ctrl Pts',(-6.66439394215464,17.1834464391567,55.8134832037256));
#6910=CARTESIAN_POINT('Ctrl Pts',(-6.66439394215464,17.1179065063808,56.1533678453107));
#6911=CARTESIAN_POINT('Ctrl Pts',(-6.66439394215464,17.0393571919978,56.5042821882919));
#6912=CARTESIAN_POINT('Ctrl Pts',(-6.66439394215464,16.9519317108386,56.8453440034822));
#6913=CARTESIAN_POINT('Ctrl Pts',(-7.2908511525663,17.3005631050862,55.8360668026084));
#6914=CARTESIAN_POINT('Ctrl Pts',(-7.2908511525663,17.2345800028592,56.1782496841166));
#6915=CARTESIAN_POINT('Ctrl Pts',(-7.2908511525663,17.1554870860676,56.531592408039));
#6916=CARTESIAN_POINT('Ctrl Pts',(-7.2908511525663,17.0674704492441,56.8749604229925));
#6917=CARTESIAN_POINT('Ctrl Pts',(-8.04465868351329,17.8781931999001,55.9474511752792));
#6918=CARTESIAN_POINT('Ctrl Pts',(-8.04465868351329,17.810004971711,56.3010696566657));
#6919=CARTESIAN_POINT('Ctrl Pts',(-8.04465868351329,17.7282761750909,56.6661880879725));
#6920=CARTESIAN_POINT('Ctrl Pts',(-8.04465868351329,17.6373180613679,57.0210313094374));
#6921=CARTESIAN_POINT('Ctrl Pts',(-8.43400087015911,18.6073592698178,56.088056219926));
#6922=CARTESIAN_POINT('Ctrl Pts',(-8.43400087015911,18.5363887387313,56.4561034927842));
#6923=CARTESIAN_POINT('Ctrl Pts',(-8.43400087015911,18.4513294878821,56.8361005713277));
#6924=CARTESIAN_POINT('Ctrl Pts',(-8.43400087015911,18.3566599854035,57.2054225576683));
#6925=CARTESIAN_POINT('Ctrl Pts',(-8.5,19.055985148285,56.1745647181597));
#6926=CARTESIAN_POINT('Ctrl Pts',(-8.5,18.9833051386494,56.551477204626));
#6927=CARTESIAN_POINT('Ctrl Pts',(-8.5,18.8961912931089,56.9406530010384));
#6928=CARTESIAN_POINT('Ctrl Pts',(-8.5,18.7992414711618,57.3188709052149));
#6929=CARTESIAN_POINT('Ctrl Pts',(-8.5,19.2663946965195,56.2151379773172));
#6930=CARTESIAN_POINT('Ctrl Pts',(-8.5,19.1929115242437,56.5962155984512));
#6931=CARTESIAN_POINT('Ctrl Pts',(-8.5,19.1048373273922,56.989681729992));
#6932=CARTESIAN_POINT('Ctrl Pts',(-8.5,19.0068161451721,57.3720791945735));
#6933=CARTESIAN_POINT('',(-8.5,19.0068161428526,57.3720791939789));
#6934=CARTESIAN_POINT('',(-6.37867965644035,16.9519317108386,56.8453440034822));
#6935=CARTESIAN_POINT('Ctrl Pts',(-8.5,19.0068161451721,57.3720791945735));
#6936=CARTESIAN_POINT('Ctrl Pts',(-8.5,18.7992414711618,57.3188709052149));
#6937=CARTESIAN_POINT('Ctrl Pts',(-8.43400087015911,18.3566599854035,57.2054225576683));
#6938=CARTESIAN_POINT('Ctrl Pts',(-8.04465868351329,17.6373180613679,57.0210313094374));
#6939=CARTESIAN_POINT('Ctrl Pts',(-7.2908511525663,17.0674704492441,56.8749604229925));
#6940=CARTESIAN_POINT('Ctrl Pts',(-6.66439394215464,16.9519317108386,56.8453440034822));
#6941=CARTESIAN_POINT('Ctrl Pts',(-6.37867965644035,16.9519317108386,56.8453440034822));
#6942=CARTESIAN_POINT('Ctrl Pts',(-6.37867965644035,16.9519317108386,56.8453440034822));
#6943=CARTESIAN_POINT('Ctrl Pts',(-6.37867965644035,17.0393555263014,56.5042886864595));
#6944=CARTESIAN_POINT('Ctrl Pts',(-6.37867965644035,17.1179077550972,56.1533613695715));
#6945=CARTESIAN_POINT('Ctrl Pts',(-6.37867965644035,17.1834464391567,55.8134832037256));
#6946=CARTESIAN_POINT('Ctrl Pts',(-8.5,19.2663946965195,56.2151379773172));
#6947=CARTESIAN_POINT('Ctrl Pts',(-8.5,19.1929115242437,56.5962155984512));
#6948=CARTESIAN_POINT('Ctrl Pts',(-8.5,19.1048373273922,56.989681729992));
#6949=CARTESIAN_POINT('Ctrl Pts',(-8.5,19.0068161451721,57.3720791945735));
#6950=CARTESIAN_POINT('Ctrl Pts',(-6.37867965629528,16.9519317107165,56.8453440039586));
#6951=CARTESIAN_POINT('Ctrl Pts',(-6.34395902543105,16.3625204948522,59.144738373737));
#6952=CARTESIAN_POINT('Ctrl Pts',(-7.21813179282277,14.2180407656508,63.4520143249812));
#6953=CARTESIAN_POINT('Ctrl Pts',(-9.58480819189232,9.76913766486894,67.3440245597847));
#6954=CARTESIAN_POINT('Ctrl Pts',(-11.1910106295689,5.89018091675158,69.0834726889151));
#6955=CARTESIAN_POINT('Ctrl Pts',(-11.9050643746374,3.17270779483425,69.7523377363836));
#6956=CARTESIAN_POINT('Ctrl Pts',(-12.3068239762497,0.360377317317033,70.0979661217499));
#6957=CARTESIAN_POINT('Ctrl Pts',(-11.9786204675957,-3.91310591747159,69.8333384317106));
#6958=CARTESIAN_POINT('Ctrl Pts',(-9.87906744362539,-9.2039373346128,67.8305030724374));
#6959=CARTESIAN_POINT('Ctrl Pts',(-7.21891300399149,-14.2217863750276,63.4517614180996));
#6960=CARTESIAN_POINT('Ctrl Pts',(-6.34395902430692,-16.3625204986098,59.1447383644959));
#6961=CARTESIAN_POINT('Ctrl Pts',(-6.37867965644035,-16.9519317131792,56.8453439943512));
#6962=CARTESIAN_POINT('Ctrl Pts',(-6.66439394200957,16.9519317107543,56.8453440038109));
#6963=CARTESIAN_POINT('Ctrl Pts',(-6.62986367742403,16.3714433629399,59.1096805950205));
#6964=CARTESIAN_POINT('Ctrl Pts',(-7.48958295564451,14.2715353296098,63.3702716486415));
#6965=CARTESIAN_POINT('Ctrl Pts',(-9.84565213340604,9.86818195374051,67.2799680929364));
#6966=CARTESIAN_POINT('Ctrl Pts',(-11.4608448228196,5.9819769902233,69.0529723976167));
#6967=CARTESIAN_POINT('Ctrl Pts',(-12.1847303919658,3.23320277617613,69.7424124829677));
#6968=CARTESIAN_POINT('Ctrl Pts',(-12.5957628559963,0.369524021153959,70.1025590335402));
#6969=CARTESIAN_POINT('Ctrl Pts',(-12.2570349822639,-3.99701914926913,69.8237052527086));
#6970=CARTESIAN_POINT('Ctrl Pts',(-10.137439575499,-9.30863506754452,67.7676071711941));
#6971=CARTESIAN_POINT('Ctrl Pts',(-7.49094960148944,-14.2753080106798,63.3705284326759));
#6972=CARTESIAN_POINT('Ctrl Pts',(-6.62986367631848,-16.3714433666239,59.109680585902));
#6973=CARTESIAN_POINT('Ctrl Pts',(-6.66439394215464,-16.9519317131792,56.8453439943512));
#6974=CARTESIAN_POINT('Ctrl Pts',(-7.29085681341187,17.0674727965435,56.8749610246921));
#6975=CARTESIAN_POINT('Ctrl Pts',(-7.25359142535474,16.5011002158146,59.0765726044006));
#6976=CARTESIAN_POINT('Ctrl Pts',(-8.07001397882514,14.4728073863862,63.2637523438959));
#6977=CARTESIAN_POINT('Ctrl Pts',(-10.3873011914576,10.1189189924078,67.2196144493972));
#6978=CARTESIAN_POINT('Ctrl Pts',(-12.0137632580413,6.19168605657765,69.0537975629472));
#6979=CARTESIAN_POINT('Ctrl Pts',(-12.7544345720524,3.36676906315595,69.779846800734));
#6980=CARTESIAN_POINT('Ctrl Pts',(-13.1824675433198,0.388852912794903,70.1655117313478));
#6981=CARTESIAN_POINT('Ctrl Pts',(-12.8242733539201,-4.17885251122572,69.8615705277069));
#6982=CARTESIAN_POINT('Ctrl Pts',(-10.6715137743796,-9.56519084510394,67.7113211237085));
#6983=CARTESIAN_POINT('Ctrl Pts',(-8.07251448834307,-14.4767690396738,63.2649464971057));
#6984=CARTESIAN_POINT('Ctrl Pts',(-7.25359142431386,-16.501100219378,59.0765725954899));
#6985=CARTESIAN_POINT('Ctrl Pts',(-7.29085681356742,-17.0674727989103,56.8749610154928));
#6986=CARTESIAN_POINT('Ctrl Pts',(-8.04466071039456,17.6373186387505,57.0210314570503));
#6987=CARTESIAN_POINT('Ctrl Pts',(-8.00890511329239,17.0603716343414,59.203097681082));
#6988=CARTESIAN_POINT('Ctrl Pts',(-8.79506791017244,15.0063077361413,63.3716260613067));
#6989=CARTESIAN_POINT('Ctrl Pts',(-11.0922237167727,10.5809826490206,67.3627780794766));
#6990=CARTESIAN_POINT('Ctrl Pts',(-12.7477737887617,6.53503905510173,69.2428293068738));
#6991=CARTESIAN_POINT('Ctrl Pts',(-13.5171077521835,3.57586091281896,69.9979929341239));
#6992=CARTESIAN_POINT('Ctrl Pts',(-13.9714915825714,0.417585392783423,70.4051811242831));
#6993=CARTESIAN_POINT('Ctrl Pts',(-13.5838871253004,-4.45711569224503,70.0794076087635));
#6994=CARTESIAN_POINT('Ctrl Pts',(-11.3703804176736,-10.0175009980528,67.8568949792364));
#6995=CARTESIAN_POINT('Ctrl Pts',(-8.79918909864043,-15.0105616090737,63.3737788829551));
#6996=CARTESIAN_POINT('Ctrl Pts',(-8.00890511229057,-17.0603716379541,59.2030976722323));
#6997=CARTESIAN_POINT('Ctrl Pts',(-8.04466071054412,-17.637318641161,57.0210314479333));
#6998=CARTESIAN_POINT('Ctrl Pts',(-8.4340034697139,18.3566600404711,57.2054225712016));
#6999=CARTESIAN_POINT('Ctrl Pts',(-8.4131142502009,17.7531399341081,59.4333522781253));
#7000=CARTESIAN_POINT('Ctrl Pts',(-9.25473584961778,15.6047661069344,63.6632982361135));
#7001=CARTESIAN_POINT('Ctrl Pts',(-11.6235485907392,11.0496166725652,67.6613555550095));
#7002=CARTESIAN_POINT('Ctrl Pts',(-13.3433740013405,6.86931369540524,69.5540876559054));
#7003=CARTESIAN_POINT('Ctrl Pts',(-14.1539310599708,3.77606032687716,70.3194772832757));
#7004=CARTESIAN_POINT('Ctrl Pts',(-14.640309711713,0.444537213945822,70.7360626019776));
#7005=CARTESIAN_POINT('Ctrl Pts',(-14.2193675814448,-4.72121257881821,70.4000180814526));
#7006=CARTESIAN_POINT('Ctrl Pts',(-11.9071685821935,-10.4691197613114,68.1548863776572));
#7007=CARTESIAN_POINT('Ctrl Pts',(-9.260484524673,-15.6092803900723,63.6659970008699));
#7008=CARTESIAN_POINT('Ctrl Pts',(-8.41311424910159,-17.7531399378894,59.4333522691111));
#7009=CARTESIAN_POINT('Ctrl Pts',(-8.43400346980125,-18.3566600429926,57.205422561893));
#7010=CARTESIAN_POINT('Ctrl Pts',(-8.49999999997069,18.7992414711669,57.3188709046107));
#7011=CARTESIAN_POINT('Ctrl Pts',(-8.49299518410109,18.1792591692181,59.5977676897671));
#7012=CARTESIAN_POINT('Ctrl Pts',(-9.40272281752661,15.9716471367371,63.9019111675863));
#7013=CARTESIAN_POINT('Ctrl Pts',(-11.8654901989597,11.3347117740451,67.9082032467995));
#7014=CARTESIAN_POINT('Ctrl Pts',(-13.6485420048835,7.07174259115336,69.8004362117152));
#7015=CARTESIAN_POINT('Ctrl Pts',(-14.4941330672572,3.89706591383746,70.5665966564561));
#7016=CARTESIAN_POINT('Ctrl Pts',(-15.0053202848577,0.4607752223178,70.9850969586586));
#7017=CARTESIAN_POINT('Ctrl Pts',(-14.5597383973889,-4.8806191580855,70.6464457045767));
#7018=CARTESIAN_POINT('Ctrl Pts',(-12.1586585520426,-10.7435452304658,68.4020692991085));
#7019=CARTESIAN_POINT('Ctrl Pts',(-9.40952176374036,-15.9763233391107,63.9048466218829));
#7020=CARTESIAN_POINT('Ctrl Pts',(-8.49299518288957,-18.1792591731044,59.5977676805651));
#7021=CARTESIAN_POINT('Ctrl Pts',(-8.5,-18.7992414737574,57.3188708950889));
#7022=CARTESIAN_POINT('Ctrl Pts',(-8.5,19.0068161451757,57.3720791939752));
#7023=CARTESIAN_POINT('Ctrl Pts',(-8.5000000012708,18.3795907455684,59.6791628056302));
#7024=CARTESIAN_POINT('Ctrl Pts',(-9.44624036508731,16.1467970192983,64.026720059828));
#7025=CARTESIAN_POINT('Ctrl Pts',(-11.9649851410576,11.4734910366497,68.0424265260941));
#7026=CARTESIAN_POINT('Ctrl Pts',(-13.7856701385902,7.17121819021727,69.9345670496955));
#7027=CARTESIAN_POINT('Ctrl Pts',(-14.6514601964537,3.95675939413664,70.7007389799831));
#7028=CARTESIAN_POINT('Ctrl Pts',(-15.1765964061977,0.468832098437293,71.119759719284));
#7029=CARTESIAN_POINT('Ctrl Pts',(-14.7173999119069,-4.95944961184219,70.7802866584454));
#7030=CARTESIAN_POINT('Ctrl Pts',(-12.2640711444334,-10.8775402354315,68.5371535059029));
#7031=CARTESIAN_POINT('Ctrl Pts',(-9.45356730467222,-16.1515515068563,64.0297644640651));
#7032=CARTESIAN_POINT('Ctrl Pts',(-8.5,-18.3795907494999,59.6791627963227));
#7033=CARTESIAN_POINT('Ctrl Pts',(-8.5,-19.0068161477964,57.3720791843357));
#7034=CARTESIAN_POINT('',(-8.49999999999999,-19.0068161477964,57.3720791843357));
#7035=CARTESIAN_POINT('',(-6.37867965644035,-16.9519317131792,56.8453439943512));
#7036=CARTESIAN_POINT('Ctrl Pts',(-8.5,-19.0068161477964,57.3720791843357));
#7037=CARTESIAN_POINT('Ctrl Pts',(-8.5,-18.7992414737574,57.3188708950889));
#7038=CARTESIAN_POINT('Ctrl Pts',(-8.43400346980125,-18.3566600429926,57.205422561893));
#7039=CARTESIAN_POINT('Ctrl Pts',(-8.04466071054412,-17.637318641161,57.0210314479333));
#7040=CARTESIAN_POINT('Ctrl Pts',(-7.29085681356742,-17.0674727989103,56.8749610154928));
#7041=CARTESIAN_POINT('Ctrl Pts',(-6.66439394215464,-16.9519317131792,56.8453439943512));
#7042=CARTESIAN_POINT('Ctrl Pts',(-6.37867965644035,-16.9519317131792,56.8453439943512));
#7043=CARTESIAN_POINT('Ctrl Pts',(-6.37867965644035,-16.9519317131792,56.8453439943512));
#7044=CARTESIAN_POINT('Ctrl Pts',(-6.34395902430692,-16.3625204986098,59.1447383644959));
#7045=CARTESIAN_POINT('Ctrl Pts',(-7.21891300399149,-14.2217863750276,63.4517614180996));
#7046=CARTESIAN_POINT('Ctrl Pts',(-9.87906744362539,-9.2039373346128,67.8305030724374));
#7047=CARTESIAN_POINT('Ctrl Pts',(-11.9786204675957,-3.91310591747159,69.8333384317106));
#7048=CARTESIAN_POINT('Ctrl Pts',(-12.3068239762497,0.360377317317033,70.0979661217499));
#7049=CARTESIAN_POINT('Ctrl Pts',(-11.9050643746374,3.17270779483425,69.7523377363836));
#7050=CARTESIAN_POINT('Ctrl Pts',(-11.1910106295689,5.89018091675158,69.0834726889151));
#7051=CARTESIAN_POINT('Ctrl Pts',(-9.58480819189232,9.76913766486894,67.3440245597847));
#7052=CARTESIAN_POINT('Ctrl Pts',(-7.21813179282277,14.2180407656508,63.4520143249812));
#7053=CARTESIAN_POINT('Ctrl Pts',(-6.34395902543105,16.3625204948522,59.144738373737));
#7054=CARTESIAN_POINT('Ctrl Pts',(-6.37867965629528,16.9519317107165,56.8453440039586));
#7055=CARTESIAN_POINT('Ctrl Pts',(-8.5,19.0068161451757,57.3720791939752));
#7056=CARTESIAN_POINT('Ctrl Pts',(-8.5000000012708,18.3795907455684,59.6791628056302));
#7057=CARTESIAN_POINT('Ctrl Pts',(-9.44624036508731,16.1467970192983,64.026720059828));
#7058=CARTESIAN_POINT('Ctrl Pts',(-11.9649851410576,11.4734910366497,68.0424265260941));
#7059=CARTESIAN_POINT('Ctrl Pts',(-13.7856701385902,7.17121819021727,69.9345670496955));
#7060=CARTESIAN_POINT('Ctrl Pts',(-14.6514601964537,3.95675939413664,70.7007389799831));
#7061=CARTESIAN_POINT('Ctrl Pts',(-15.1765964061977,0.468832098437293,71.119759719284));
#7062=CARTESIAN_POINT('Ctrl Pts',(-14.7173999119069,-4.95944961184219,70.7802866584454));
#7063=CARTESIAN_POINT('Ctrl Pts',(-12.2640711444334,-10.8775402354315,68.5371535059029));
#7064=CARTESIAN_POINT('Ctrl Pts',(-9.45356730467222,-16.1515515068563,64.0297644640651));
#7065=CARTESIAN_POINT('Ctrl Pts',(-8.5,-18.3795907494999,59.6791627963227));
#7066=CARTESIAN_POINT('Ctrl Pts',(-8.5,-19.0068161477964,57.3720791843357));
#7067=CARTESIAN_POINT('Ctrl Pts',(-6.37867965644035,-16.9519317131792,56.8453439943512));
#7068=CARTESIAN_POINT('Ctrl Pts',(-6.37867965644035,-17.0393555276599,56.504288680396));
#7069=CARTESIAN_POINT('Ctrl Pts',(-6.37867965644035,-17.117907755524,56.153361367358));
#7070=CARTESIAN_POINT('Ctrl Pts',(-6.37867965644035,-17.1834464391567,55.8134832037256));
#7071=CARTESIAN_POINT('Ctrl Pts',(-6.66439394215464,-16.9519317131792,56.8453439943512));
#7072=CARTESIAN_POINT('Ctrl Pts',(-6.66439394215464,-17.0393571933563,56.5042821822285));
#7073=CARTESIAN_POINT('Ctrl Pts',(-6.66439394215464,-17.1179065068077,56.1533678430972));
#7074=CARTESIAN_POINT('Ctrl Pts',(-6.66439394215464,-17.1834464391567,55.8134832037256));
#7075=CARTESIAN_POINT('Ctrl Pts',(-7.29085115256629,-17.0674704516006,56.8749604137993));
#7076=CARTESIAN_POINT('Ctrl Pts',(-7.29085115256629,-17.1554870874354,56.5315924019341));
#7077=CARTESIAN_POINT('Ctrl Pts',(-7.29085115256629,-17.2345800032889,56.178249681888));
#7078=CARTESIAN_POINT('Ctrl Pts',(-7.29085115256629,-17.3005631050862,55.8360668026083));
#7079=CARTESIAN_POINT('Ctrl Pts',(-8.04465868351329,-17.6373180638031,57.0210312999373));
#7080=CARTESIAN_POINT('Ctrl Pts',(-8.04465868351329,-17.7282761765043,56.6661880816638));
#7081=CARTESIAN_POINT('Ctrl Pts',(-8.04465868351328,-17.8100049721551,56.3010696543627));
#7082=CARTESIAN_POINT('Ctrl Pts',(-8.04465868351328,-17.8781931999001,55.9474511752791));
#7083=CARTESIAN_POINT('Ctrl Pts',(-8.43400087015911,-18.356659987938,57.2054225477807));
#7084=CARTESIAN_POINT('Ctrl Pts',(-8.43400087015911,-18.4513294893531,56.8361005647618));
#7085=CARTESIAN_POINT('Ctrl Pts',(-8.43400087015911,-18.5363887391935,56.4561034903872));
#7086=CARTESIAN_POINT('Ctrl Pts',(-8.43400087015911,-18.6073592698178,56.0880562199259));
#7087=CARTESIAN_POINT('Ctrl Pts',(-8.5,-18.7992414737574,57.3188708950889));
#7088=CARTESIAN_POINT('Ctrl Pts',(-8.5,-18.8961912946155,56.9406529943141));
#7089=CARTESIAN_POINT('Ctrl Pts',(-8.5,-18.9833051391228,56.5514772021713));
#7090=CARTESIAN_POINT('Ctrl Pts',(-8.5,-19.055985148285,56.1745647181597));
#7091=CARTESIAN_POINT('Ctrl Pts',(-8.5,-19.0068161477963,57.3720791843357));
#7092=CARTESIAN_POINT('Ctrl Pts',(-8.5,-19.1048373289154,56.9896817231935));
#7093=CARTESIAN_POINT('Ctrl Pts',(-8.5,-19.1929115247223,56.5962155959693));
#7094=CARTESIAN_POINT('Ctrl Pts',(-8.5,-19.2663946965195,56.2151379773172));
#7095=CARTESIAN_POINT('',(-8.5,-19.2663946965195,56.2151379773172));
#7096=CARTESIAN_POINT('',(-6.37867965644035,-17.1834464391567,55.8134832037256));
#7097=CARTESIAN_POINT('Ctrl Pts',(-8.5,-19.2663946965195,56.2151379773172));
#7098=CARTESIAN_POINT('Ctrl Pts',(-8.5,-19.055985148285,56.1745647181597));
#7099=CARTESIAN_POINT('Ctrl Pts',(-8.43400087015911,-18.6073592698178,56.0880562199259));
#7100=CARTESIAN_POINT('Ctrl Pts',(-8.04465868351328,-17.8781931999001,55.9474511752791));
#7101=CARTESIAN_POINT('Ctrl Pts',(-7.29085115256629,-17.3005631050862,55.8360668026083));
#7102=CARTESIAN_POINT('Ctrl Pts',(-6.66439394215464,-17.1834464391567,55.8134832037256));
#7103=CARTESIAN_POINT('Ctrl Pts',(-6.37867965644035,-17.1834464391567,55.8134832037256));
#7104=CARTESIAN_POINT('Ctrl Pts',(-6.37867965644035,-17.1834464391567,55.8134832037256));
#7105=CARTESIAN_POINT('Ctrl Pts',(-6.37867965644035,-17.117907755524,56.153361367358));
#7106=CARTESIAN_POINT('Ctrl Pts',(-6.37867965644035,-17.0393555276599,56.504288680396));
#7107=CARTESIAN_POINT('Ctrl Pts',(-6.37867965644035,-16.9519317131792,56.8453439943512));
#7108=CARTESIAN_POINT('Ctrl Pts',(-8.5,-19.0068161477963,57.3720791843357));
#7109=CARTESIAN_POINT('Ctrl Pts',(-8.5,-19.1048373289154,56.9896817231935));
#7110=CARTESIAN_POINT('Ctrl Pts',(-8.5,-19.1929115247223,56.5962155959693));
#7111=CARTESIAN_POINT('Ctrl Pts',(-8.5,-19.2663946965195,56.2151379773172));
#7112=CARTESIAN_POINT('Ctrl Pts',(-6.37867965644035,-17.1834464391566,55.8134832037259));
#7113=CARTESIAN_POINT('Ctrl Pts',(-6.37867965644035,-17.2671029617921,55.3796474335628));
#7114=CARTESIAN_POINT('Ctrl Pts',(-6.37867965644035,-17.7670670675718,54.4348084088707));
#7115=CARTESIAN_POINT('Ctrl Pts',(-6.37867965644035,-18.7797191983724,54.));
#7116=CARTESIAN_POINT('Ctrl Pts',(-6.37867965644035,-19.3800314873921,54.));
#7117=CARTESIAN_POINT('Ctrl Pts',(-6.66439394215464,-17.1834464391566,55.8134832037259));
#7118=CARTESIAN_POINT('Ctrl Pts',(-6.66439394215464,-17.2670904928921,55.3797120962412));
#7119=CARTESIAN_POINT('Ctrl Pts',(-6.66439394215464,-17.7670945835653,54.4349191596844));
#7120=CARTESIAN_POINT('Ctrl Pts',(-6.66439394215464,-18.7798086741675,54.));
#7121=CARTESIAN_POINT('Ctrl Pts',(-6.66439394215464,-19.3800314873921,54.));
#7122=CARTESIAN_POINT('Ctrl Pts',(-7.29085029793426,-17.3005627451802,55.836066733208));
#7123=CARTESIAN_POINT('Ctrl Pts',(-7.29085029793426,-17.3797815861421,55.4252444112012));
#7124=CARTESIAN_POINT('Ctrl Pts',(-7.29085029793426,-17.8530161833129,54.5306979949696));
#7125=CARTESIAN_POINT('Ctrl Pts',(-7.29085029793426,-18.811563635118,54.1192738233666));
#7126=CARTESIAN_POINT('Ctrl Pts',(-7.29085029793426,-19.3800314873921,54.1192738233666));
#7127=CARTESIAN_POINT('Ctrl Pts',(-8.04465837989033,-17.8781931120305,55.9474511583355));
#7128=CARTESIAN_POINT('Ctrl Pts',(-8.04465837989033,-17.9353929452527,55.6508175795378));
#7129=CARTESIAN_POINT('Ctrl Pts',(-8.04465837989033,-18.277217601953,55.0048072380441));
#7130=CARTESIAN_POINT('Ctrl Pts',(-8.04465837989033,-18.9695702139447,54.7075453005509));
#7131=CARTESIAN_POINT('Ctrl Pts',(-8.04465837989033,-19.3800314873921,54.7075453005509));
#7132=CARTESIAN_POINT('Ctrl Pts',(-8.43400047932411,-18.6073592624962,56.0880562185142));
#7133=CARTESIAN_POINT('Ctrl Pts',(-8.43400047932411,-18.6367767603382,55.9354995208353));
#7134=CARTESIAN_POINT('Ctrl Pts',(-8.43400047932411,-18.8126751779652,55.6031777109637));
#7135=CARTESIAN_POINT('Ctrl Pts',(-8.43400047932411,-19.1689339553594,55.4501441545311));
#7136=CARTESIAN_POINT('Ctrl Pts',(-8.43400047932411,-19.3800314873921,55.4501441545311));
#7137=CARTESIAN_POINT('Ctrl Pts',(-8.5,-19.055985148285,56.1745647181597));
#7138=CARTESIAN_POINT('Ctrl Pts',(-8.5,-19.0683328632447,56.1105304951182));
#7139=CARTESIAN_POINT('Ctrl Pts',(-8.5,-19.1420682054501,55.9711212909647));
#7140=CARTESIAN_POINT('Ctrl Pts',(-8.5,-19.291425305852,55.9070346292739));
#7141=CARTESIAN_POINT('Ctrl Pts',(-8.5,-19.3800314873921,55.9070346292739));
#7142=CARTESIAN_POINT('Ctrl Pts',(-8.5,-19.2663946965196,56.2151379773172));
#7143=CARTESIAN_POINT('Ctrl Pts',(-8.5,-19.2707225320274,56.1926941822423));
#7144=CARTESIAN_POINT('Ctrl Pts',(-8.5,-19.2965873700759,56.143814456532));
#7145=CARTESIAN_POINT('Ctrl Pts',(-8.5,-19.3489752976487,56.1213203435596));
#7146=CARTESIAN_POINT('Ctrl Pts',(-8.5,-19.3800314873921,56.1213203435596));
#7147=CARTESIAN_POINT('',(-8.5,-19.3800314873921,56.1213203435596));
#7148=CARTESIAN_POINT('',(-6.37867965644035,-19.3800314873921,54.));
#7149=CARTESIAN_POINT('Ctrl Pts',(-8.5,-19.3800314873921,56.1213203435596));
#7150=CARTESIAN_POINT('Ctrl Pts',(-8.5,-19.3800314873921,55.9070346292739));
#7151=CARTESIAN_POINT('Ctrl Pts',(-8.43400047932411,-19.3800314873921,55.4501441545311));
#7152=CARTESIAN_POINT('Ctrl Pts',(-8.04465837989033,-19.3800314873921,54.7075453005509));
#7153=CARTESIAN_POINT('Ctrl Pts',(-7.29085029793426,-19.3800314873921,54.1192738233666));
#7154=CARTESIAN_POINT('Ctrl Pts',(-6.66439394215464,-19.3800314873921,54.));
#7155=CARTESIAN_POINT('Ctrl Pts',(-6.37867965644035,-19.3800314873921,54.));
#7156=CARTESIAN_POINT('Ctrl Pts',(-6.37867965644035,-19.3800314873921,54.));
#7157=CARTESIAN_POINT('Ctrl Pts',(-6.37867965644035,-18.7797191983724,54.));
#7158=CARTESIAN_POINT('Ctrl Pts',(-6.37867965644035,-17.7670670675718,54.4348084088707));
#7159=CARTESIAN_POINT('Ctrl Pts',(-6.37867965644035,-17.2671029617921,55.3796474335628));
#7160=CARTESIAN_POINT('Ctrl Pts',(-6.37867965644035,-17.1834464391566,55.8134832037259));
#7161=CARTESIAN_POINT('Ctrl Pts',(-8.5,-19.2663946965196,56.2151379773172));
#7162=CARTESIAN_POINT('Ctrl Pts',(-8.5,-19.2707225320274,56.1926941822423));
#7163=CARTESIAN_POINT('Ctrl Pts',(-8.5,-19.2965873700759,56.143814456532));
#7164=CARTESIAN_POINT('Ctrl Pts',(-8.5,-19.3489752976487,56.1213203435596));
#7165=CARTESIAN_POINT('Ctrl Pts',(-8.5,-19.3800314873921,56.1213203435596));
#7166=CARTESIAN_POINT('Ctrl Pts',(-6.37867965644035,-19.380031542032,54.));
#7167=CARTESIAN_POINT('Ctrl Pts',(-6.37867965644035,-23.5940881839923,54.0000002170871));
#7168=CARTESIAN_POINT('Ctrl Pts',(-6.37867965644035,-27.7891699875342,54.0000004331968));
#7169=CARTESIAN_POINT('Ctrl Pts',(-6.37867965644035,-31.999999845455,54.0000006501177));
#7170=CARTESIAN_POINT('Ctrl Pts',(-6.66439394215464,-19.380031542032,54.));
#7171=CARTESIAN_POINT('Ctrl Pts',(-6.66439394215464,-23.5940881839923,54.0000002170871));
#7172=CARTESIAN_POINT('Ctrl Pts',(-6.66439394215464,-27.7891699875342,54.0000004331968));
#7173=CARTESIAN_POINT('Ctrl Pts',(-6.66439394215464,-31.999999845455,54.0000006501177));
#7174=CARTESIAN_POINT('Ctrl Pts',(-7.29086126549403,-19.3800315358874,54.1192785130262));
#7175=CARTESIAN_POINT('Ctrl Pts',(-7.29086126549403,-23.5940881778477,54.1192787301133));
#7176=CARTESIAN_POINT('Ctrl Pts',(-7.29086126549403,-27.7891699813896,54.1192789462229));
#7177=CARTESIAN_POINT('Ctrl Pts',(-7.29086126549403,-31.9999998393104,54.1192791631438));
#7178=CARTESIAN_POINT('Ctrl Pts',(-8.04466232388412,-19.3800315055827,54.7075464587638));
#7179=CARTESIAN_POINT('Ctrl Pts',(-8.04466232388412,-23.594088147543,54.707546675851));
#7180=CARTESIAN_POINT('Ctrl Pts',(-8.04466232388412,-27.789169951085,54.7075468919606));
#7181=CARTESIAN_POINT('Ctrl Pts',(-8.04466232388412,-31.9999998090057,54.7075471088815));
#7182=CARTESIAN_POINT('Ctrl Pts',(-8.43400552734115,-19.3800314673278,55.4501442725561));
#7183=CARTESIAN_POINT('Ctrl Pts',(-8.43400552734115,-23.5940881092881,55.4501444896432));
#7184=CARTESIAN_POINT('Ctrl Pts',(-8.43400552734115,-27.78916991283,55.4501447057528));
#7185=CARTESIAN_POINT('Ctrl Pts',(-8.43400552734115,-31.9999997707508,55.4501449226738));
#7186=CARTESIAN_POINT('Ctrl Pts',(-8.5,-19.3800314437911,55.9070346292739));
#7187=CARTESIAN_POINT('Ctrl Pts',(-8.5,-23.5940880857514,55.9070348463611));
#7188=CARTESIAN_POINT('Ctrl Pts',(-8.5,-27.7891698892933,55.9070350624707));
#7189=CARTESIAN_POINT('Ctrl Pts',(-8.5,-31.9999997472141,55.9070352793916));
#7190=CARTESIAN_POINT('Ctrl Pts',(-8.5,-19.3800314327522,56.1213203435596));
#7191=CARTESIAN_POINT('Ctrl Pts',(-8.5,-23.5940880747125,56.1213205606468));
#7192=CARTESIAN_POINT('Ctrl Pts',(-8.5,-27.7891698782544,56.1213207767564));
#7193=CARTESIAN_POINT('Ctrl Pts',(-8.5,-31.9999997361752,56.1213209936773));
#7194=CARTESIAN_POINT('',(-8.5,-31.9999997361752,56.1213209936773));
#7195=CARTESIAN_POINT('',(-6.37867965644035,-31.999999845455,54.0000006501177));
#7196=CARTESIAN_POINT('Ctrl Pts',(-8.5,-31.9999997361752,56.1213209936773));
#7197=CARTESIAN_POINT('Ctrl Pts',(-8.5,-31.9999997472141,55.9070352793916));
#7198=CARTESIAN_POINT('Ctrl Pts',(-8.43400552734115,-31.9999997707508,55.4501449226738));
#7199=CARTESIAN_POINT('Ctrl Pts',(-8.04466232388412,-31.9999998090057,54.7075471088815));
#7200=CARTESIAN_POINT('Ctrl Pts',(-7.29086126549403,-31.9999998393104,54.1192791631438));
#7201=CARTESIAN_POINT('Ctrl Pts',(-6.66439394215464,-31.999999845455,54.0000006501177));
#7202=CARTESIAN_POINT('Ctrl Pts',(-6.37867965644035,-31.999999845455,54.0000006501177));
#7203=CARTESIAN_POINT('Ctrl Pts',(-6.37867965644035,-31.999999845455,54.0000006501177));
#7204=CARTESIAN_POINT('Ctrl Pts',(-6.37867965644035,-27.7891699875342,54.0000004331968));
#7205=CARTESIAN_POINT('Ctrl Pts',(-6.37867965644035,-23.5940881839923,54.0000002170871));
#7206=CARTESIAN_POINT('Ctrl Pts',(-6.37867965644035,-19.380031542032,54.));
#7207=CARTESIAN_POINT('Ctrl Pts',(-8.5,-19.3800314873921,56.1213203435597));
#7208=CARTESIAN_POINT('Ctrl Pts',(-8.5,-23.5940881109751,56.1213205606468));
#7209=CARTESIAN_POINT('Ctrl Pts',(-8.5,-27.7891698964537,56.1213207767564));
#7210=CARTESIAN_POINT('Ctrl Pts',(-8.5,-31.9999997361752,56.1213209936773));
#7211=CARTESIAN_POINT('Ctrl Pts',(-6.37867965644035,-31.999999845455,54.0000006501177));
#7212=CARTESIAN_POINT('Ctrl Pts',(-6.37867965644035,-32.6261158828895,54.0000006823721));
#7213=CARTESIAN_POINT('Ctrl Pts',(-6.37867965644035,-33.2502411339106,53.7979493706431));
#7214=CARTESIAN_POINT('Ctrl Pts',(-6.37867965644035,-33.7574178884678,53.4313546690326));
#7215=CARTESIAN_POINT('Ctrl Pts',(-6.66439394215464,-31.999999845455,54.0000006501177));
#7216=CARTESIAN_POINT('Ctrl Pts',(-6.66439394215464,-32.6261854714262,54.0000006823756));
#7217=CARTESIAN_POINT('Ctrl Pts',(-6.66439394215464,-33.2501847646659,53.7979901151494));
#7218=CARTESIAN_POINT('Ctrl Pts',(-6.66439394215464,-33.7574178884678,53.4313546690326));
#7219=CARTESIAN_POINT('Ctrl Pts',(-7.29086279675178,-31.9999998393103,54.1192798154656));
#7220=CARTESIAN_POINT('Ctrl Pts',(-7.29086279675178,-32.6508824379237,54.1192798489958));
#7221=CARTESIAN_POINT('Ctrl Pts',(-7.29086279675178,-33.3000537651981,53.9091203003576));
#7222=CARTESIAN_POINT('Ctrl Pts',(-7.29086279675178,-33.8272923347691,53.5280246283797));
#7223=CARTESIAN_POINT('Ctrl Pts',(-8.04466288268867,-31.9999998090057,54.7075472722757));
#7224=CARTESIAN_POINT('Ctrl Pts',(-8.04466288268867,-32.7737697939603,54.7075473121365));
#7225=CARTESIAN_POINT('Ctrl Pts',(-8.04466288268867,-33.545121098274,54.4578337518026));
#7226=CARTESIAN_POINT('Ctrl Pts',(-8.04466288268867,-34.1719029187029,54.0047867768171));
#7227=CARTESIAN_POINT('Ctrl Pts',(-8.43400623770282,-31.9999997707508,55.4501449429846));
#7228=CARTESIAN_POINT('Ctrl Pts',(-8.43400623770282,-32.9288220914724,55.4501449908329));
#7229=CARTESIAN_POINT('Ctrl Pts',(-8.43400623770282,-33.854541212412,55.1504571029839));
#7230=CARTESIAN_POINT('Ctrl Pts',(-8.43400623770282,-34.6069210621824,54.6066260538554));
#7231=CARTESIAN_POINT('Ctrl Pts',(-8.5,-31.9999997472141,55.9070352793916));
#7232=CARTESIAN_POINT('Ctrl Pts',(-8.5,-33.0240879867551,55.9070353321475));
#7233=CARTESIAN_POINT('Ctrl Pts',(-8.49999999999999,-34.0450214379272,55.5765232560171));
#7234=CARTESIAN_POINT('Ctrl Pts',(-8.49999999999999,-34.8745701456056,54.9769134390642));
#7235=CARTESIAN_POINT('Ctrl Pts',(-8.5,-31.9999997361752,56.1213209936773));
#7236=CARTESIAN_POINT('Ctrl Pts',(-8.5,-33.0688466694893,56.121321048739));
#7237=CARTESIAN_POINT('Ctrl Pts',(-8.5,-34.1342951178172,55.7763978843389));
#7238=CARTESIAN_POINT('Ctrl Pts',(-8.5,-35.0000999947819,55.1505815832724));
#7239=CARTESIAN_POINT('',(-8.5,-35.000099996118,55.1505815851209));
#7240=CARTESIAN_POINT('',(-6.37867965644035,-33.7574178884678,53.4313546690326));
#7241=CARTESIAN_POINT('Ctrl Pts',(-8.5,-35.0000999947819,55.1505815832724));
#7242=CARTESIAN_POINT('Ctrl Pts',(-8.49999999999999,-34.8745701456056,54.9769134390642));
#7243=CARTESIAN_POINT('Ctrl Pts',(-8.43400623770282,-34.6069210621824,54.6066260538554));
#7244=CARTESIAN_POINT('Ctrl Pts',(-8.04466288268867,-34.1719029187029,54.0047867768171));
#7245=CARTESIAN_POINT('Ctrl Pts',(-7.29086279675178,-33.8272923347691,53.5280246283797));
#7246=CARTESIAN_POINT('Ctrl Pts',(-6.66439394215464,-33.7574178884678,53.4313546690326));
#7247=CARTESIAN_POINT('Ctrl Pts',(-6.37867965644035,-33.7574178884678,53.4313546690326));
#7248=CARTESIAN_POINT('Ctrl Pts',(-6.37867965644035,-33.7574178884678,53.4313546690326));
#7249=CARTESIAN_POINT('Ctrl Pts',(-6.37867965644035,-33.2502411339106,53.7979493706431));
#7250=CARTESIAN_POINT('Ctrl Pts',(-6.37867965644035,-32.6261158828895,54.0000006823721));
#7251=CARTESIAN_POINT('Ctrl Pts',(-6.37867965644035,-31.999999845455,54.0000006501177));
#7252=CARTESIAN_POINT('Ctrl Pts',(-8.5,-31.9999997361752,56.1213209936773));
#7253=CARTESIAN_POINT('Ctrl Pts',(-8.5,-33.0688466694893,56.121321048739));
#7254=CARTESIAN_POINT('Ctrl Pts',(-8.5,-34.1342951178172,55.7763978843389));
#7255=CARTESIAN_POINT('Ctrl Pts',(-8.5,-35.0000999947819,55.1505815832724));
#7256=CARTESIAN_POINT('Ctrl Pts',(-6.37867965644035,-33.7574178915313,53.4313546668182));
#7257=CARTESIAN_POINT('Ctrl Pts',(-6.37867965644035,-34.0855855212474,53.1941503518879));
#7258=CARTESIAN_POINT('Ctrl Pts',(-6.37867965644035,-34.7382072200962,52.4834496268985));
#7259=CARTESIAN_POINT('Ctrl Pts',(-6.37867965644035,-35.,51.5400520046389));
#7260=CARTESIAN_POINT('Ctrl Pts',(-6.37867965644035,-35.,51.0000006501177));
#7261=CARTESIAN_POINT('Ctrl Pts',(-6.66439394215464,-33.7574178915313,53.4313546668182));
#7262=CARTESIAN_POINT('Ctrl Pts',(-6.66439394215464,-34.0856219948462,53.1941239882425));
#7263=CARTESIAN_POINT('Ctrl Pts',(-6.66439394215464,-34.7382647569064,52.4834385847507));
#7264=CARTESIAN_POINT('Ctrl Pts',(-6.66439394215464,-35.,51.5401120276717));
#7265=CARTESIAN_POINT('Ctrl Pts',(-6.66439394215464,-35.,51.0000006501177));
#7266=CARTESIAN_POINT('Ctrl Pts',(-7.29086286320516,-33.8272923545303,53.5280246490098));
#7267=CARTESIAN_POINT('Ctrl Pts',(-7.29086286320516,-34.1684409385622,53.2814375123238));
#7268=CARTESIAN_POINT('Ctrl Pts',(-7.29086286320516,-34.846972065121,52.5424514137685));
#7269=CARTESIAN_POINT('Ctrl Pts',(-7.29086286320516,-35.1192791936438,51.5614142028766));
#7270=CARTESIAN_POINT('Ctrl Pts',(-7.29086286320516,-35.1192791936438,51.0000006501177));
#7271=CARTESIAN_POINT('Ctrl Pts',(-8.04466290698454,-34.1719029266483,54.0047867798349));
#7272=CARTESIAN_POINT('Ctrl Pts',(-8.04466290698454,-34.5774607573477,53.711643706952));
#7273=CARTESIAN_POINT('Ctrl Pts',(-8.04466290698454,-35.3839980659312,52.8333217523325));
#7274=CARTESIAN_POINT('Ctrl Pts',(-8.04466290698455,-35.7075466292583,51.6674097300301));
#7275=CARTESIAN_POINT('Ctrl Pts',(-8.04466290698455,-35.7075466292583,51.0000006501177));
#7276=CARTESIAN_POINT('Ctrl Pts',(-8.43400626856183,-34.6069210672554,54.6066260513022));
#7277=CARTESIAN_POINT('Ctrl Pts',(-8.43400626856183,-35.0937468330793,54.2547413380763));
#7278=CARTESIAN_POINT('Ctrl Pts',(-8.43400626856183,-36.0618499111555,53.2005128404082));
#7279=CARTESIAN_POINT('Ctrl Pts',(-8.43400626856183,-36.4501442937695,51.8011488757254));
#7280=CARTESIAN_POINT('Ctrl Pts',(-8.43400626856183,-36.4501442937695,51.0000006501177));
#7281=CARTESIAN_POINT('Ctrl Pts',(-8.5,-34.8745701506165,54.9769134354423));
#7282=CARTESIAN_POINT('Ctrl Pts',(-8.5,-35.4113278602056,54.588937190202));
#7283=CARTESIAN_POINT('Ctrl Pts',(-8.49999999999999,-36.4787960194463,53.4264515481114));
#7284=CARTESIAN_POINT('Ctrl Pts',(-8.5,-36.9070346292739,51.8833197281267));
#7285=CARTESIAN_POINT('Ctrl Pts',(-8.5,-36.9070346292739,51.0000006501177));
#7286=CARTESIAN_POINT('Ctrl Pts',(-8.5,-35.0001000000116,55.1505815794923));
#7287=CARTESIAN_POINT('Ctrl Pts',(-8.5,-35.560317186066,54.745648484948));
#7288=CARTESIAN_POINT('Ctrl Pts',(-8.49999999999999,-36.6744121137202,53.5324064579244));
#7289=CARTESIAN_POINT('Ctrl Pts',(-8.5,-37.1213203435596,51.9219259796098));
#7290=CARTESIAN_POINT('Ctrl Pts',(-8.5,-37.1213203435596,51.0000006501177));
#7291=CARTESIAN_POINT('',(-6.39927708632443,-35.0001000000116,51.0000006501177));
#7292=CARTESIAN_POINT('Ctrl Pts',(-8.5,-35.0001000000116,55.1505815794923));
#7293=CARTESIAN_POINT('Ctrl Pts',(-8.5,-35.0001000000116,54.7942909783228));
#7294=CARTESIAN_POINT('Ctrl Pts',(-8.44252630885498,-35.0001000000116,54.3341755321066));
#7295=CARTESIAN_POINT('Ctrl Pts',(-7.9977864749675,-35.0001000000116,53.1607439828215));
#7296=CARTESIAN_POINT('Ctrl Pts',(-7.64356066430923,-35.0001000000116,52.6053548907106));
#7297=CARTESIAN_POINT('Ctrl Pts',(-7.13512176886221,-35.0001000000116,51.9212185861545));
#7298=CARTESIAN_POINT('Ctrl Pts',(-6.98622001132231,-35.0001000000116,51.733048434934));
#7299=CARTESIAN_POINT('Ctrl Pts',(-6.77438009122045,-35.0001000000116,51.4732179267382));
#7300=CARTESIAN_POINT('Ctrl Pts',(-6.71639805957763,-35.0001000000183,51.4029135245357));
#7301=CARTESIAN_POINT('Ctrl Pts',(-6.56409934304602,-35.0001000000183,51.2192961959561));
#7302=CARTESIAN_POINT('Ctrl Pts',(-6.49554616509506,-35.0001000000116,51.1375362219706));
#7303=CARTESIAN_POINT('Ctrl Pts',(-6.421818278566,-35.0001000000116,51.0464054488998));
#7304=CARTESIAN_POINT('Ctrl Pts',(-6.40818706140854,-35.0001000000116,51.027500080116));
#7305=CARTESIAN_POINT('Ctrl Pts',(-6.40112856488211,-35.0001000000116,51.0110323238185));
#7306=CARTESIAN_POINT('Ctrl Pts',(-6.40013353150608,-35.0001000000116,51.007791289022));
#7307=CARTESIAN_POINT('Ctrl Pts',(-6.39939979873532,-35.0001000000116,51.0030753137652));
#7308=CARTESIAN_POINT('Ctrl Pts',(-6.39927708632375,-35.0001000000116,51.001544338149));
#7309=CARTESIAN_POINT('Ctrl Pts',(-6.39927708632375,-35.0001000000116,51.0000006501177));
#7310=CARTESIAN_POINT('',(-6.37867965644035,-35.,51.0000006501177));
#7311=CARTESIAN_POINT('Ctrl Pts',(-6.39927705543382,-35.0001030896936,51.0000006501177));
#7312=CARTESIAN_POINT('Ctrl Pts',(-6.39239586884655,-35.0000342828437,51.0000006501177));
#7313=CARTESIAN_POINT('Ctrl Pts',(-6.38552985288297,-35.,51.0000006501177));
#7314=CARTESIAN_POINT('Ctrl Pts',(-6.37867965644035,-35.,51.0000006501177));
#7315=CARTESIAN_POINT('Ctrl Pts',(-6.37867965644035,-35.,51.0000006501177));
#7316=CARTESIAN_POINT('Ctrl Pts',(-6.37867965644035,-35.,51.5400520046389));
#7317=CARTESIAN_POINT('Ctrl Pts',(-6.37867965644035,-34.7382072200962,52.4834496268985));
#7318=CARTESIAN_POINT('Ctrl Pts',(-6.37867965644035,-34.0855855212474,53.1941503518879));
#7319=CARTESIAN_POINT('Ctrl Pts',(-6.37867965644035,-33.7574178915313,53.4313546668182));
#7320=CARTESIAN_POINT('Ctrl Pts',(-6.37867965644035,-35.,51.0000006501177));
#7321=CARTESIAN_POINT('Ctrl Pts',(-6.37867965644035,-35.,44.3274205067641));
#7322=CARTESIAN_POINT('Ctrl Pts',(-6.37867965644035,-35.,37.6674518910119));
#7323=CARTESIAN_POINT('Ctrl Pts',(-6.37867965644035,-35.,31.));
#7324=CARTESIAN_POINT('Ctrl Pts',(-6.38553184849945,-35.,51.0000006501177));
#7325=CARTESIAN_POINT('Ctrl Pts',(-6.38553184849945,-35.,44.3274205067641));
#7326=CARTESIAN_POINT('Ctrl Pts',(-6.38553184849945,-35.,37.6674518910119));
#7327=CARTESIAN_POINT('Ctrl Pts',(-6.38553184849945,-35.,31.));
#7328=CARTESIAN_POINT('Ctrl Pts',(-6.39239779355103,-35.0000332008452,51.0000006501177));
#7329=CARTESIAN_POINT('Ctrl Pts',(-6.39239779355103,-35.0000332008452,44.3274205067641));
#7330=CARTESIAN_POINT('Ctrl Pts',(-6.39239779355103,-35.0000332008452,37.6674518910119));
#7331=CARTESIAN_POINT('Ctrl Pts',(-6.39239779355103,-35.0000332008452,31.));
#7332=CARTESIAN_POINT('Ctrl Pts',(-6.39927708632444,-35.0001000000116,51.0000006501177));
#7333=CARTESIAN_POINT('Ctrl Pts',(-6.39927708632444,-35.0001000000116,44.3274205067641));
#7334=CARTESIAN_POINT('Ctrl Pts',(-6.39927708632444,-35.0001000000116,37.6674518910119));
#7335=CARTESIAN_POINT('Ctrl Pts',(-6.39927708632444,-35.0001000000116,31.));
#7336=CARTESIAN_POINT('',(-6.37867965644035,-35.,31.));
#7337=CARTESIAN_POINT('',(-6.39927699932664,-35.0000000027982,31.));
#7338=CARTESIAN_POINT('',(-20.,-35.,31.));
#7339=CARTESIAN_POINT('Ctrl Pts',(-6.37867965644035,-35.,31.));
#7340=CARTESIAN_POINT('Ctrl Pts',(-6.37867965644035,-35.,37.6674518910119));
#7341=CARTESIAN_POINT('Ctrl Pts',(-6.37867965644035,-35.,44.3274205067641));
#7342=CARTESIAN_POINT('Ctrl Pts',(-6.37867965644035,-35.,51.0000006501177));
#7343=CARTESIAN_POINT('Ctrl Pts',(-6.39927708632407,-35.0001000000116,51.0000006501177));
#7344=CARTESIAN_POINT('Ctrl Pts',(-6.39927708632398,-35.0001000000116,46.7650241821894));
#7345=CARTESIAN_POINT('Ctrl Pts',(-6.3992770863239,-35.0001000000116,42.5300477142611));
#7346=CARTESIAN_POINT('Ctrl Pts',(-6.39927708632376,-35.0001000000116,35.8633808308886));
#7347=CARTESIAN_POINT('Ctrl Pts',(-6.39927708632391,-35.0001000000116,33.4316904154443));
#7348=CARTESIAN_POINT('Ctrl Pts',(-6.39927708632403,-35.0001000000116,31.));
#7349=CARTESIAN_POINT('Origin',(-8.5,-5.00000057890304E-5,52.9360395921679));
#7350=CARTESIAN_POINT('',(-8.5,-35.0001000000116,57.3720791843357));
#7351=CARTESIAN_POINT('',(-8.5,17.499924739221,57.3720791843357));
#7352=CARTESIAN_POINT('',(-8.5,-35.0001000000116,74.8720791843357));
#7353=CARTESIAN_POINT('Origin',(-26.,17.499924739221,57.3720791843357));
#7354=CARTESIAN_POINT('',(-8.5,34.9999395751835,57.3720791843357));
#7355=CARTESIAN_POINT('',(-8.5,17.499924739221,57.3720791843357));
#7356=CARTESIAN_POINT('',(-26.,34.9998994784478,74.8720791843345));
#7357=CARTESIAN_POINT('Origin',(-26.,34.9999395751835,57.3720791843357));
#7358=CARTESIAN_POINT('',(-26.,-35.0001000000116,74.8720791843357));
#7359=CARTESIAN_POINT('',(-26.,17.499924739221,74.8720791843357));
#7360=CARTESIAN_POINT('Origin',(-26.,-35.0001000000116,57.3720791843357));
#7361=CARTESIAN_POINT('Origin',(-8.5,-5.00000057890304E-5,52.9360395921679));
#7362=CARTESIAN_POINT('',(-8.5,34.9998994784478,74.8720791843345));
#7363=CARTESIAN_POINT('Ctrl Pts',(-2.12132034355964,35.,51.0000006501177));
#7364=CARTESIAN_POINT('Ctrl Pts',(-2.12132034355964,35.,43.9937759547244));
#7365=CARTESIAN_POINT('Ctrl Pts',(-2.12132034355964,35.,37.0008534541443));
#7366=CARTESIAN_POINT('Ctrl Pts',(-2.12132034355964,35.,30.));
#7367=CARTESIAN_POINT('Ctrl Pts',(-1.83560605784536,35.,51.0000006501177));
#7368=CARTESIAN_POINT('Ctrl Pts',(-1.83560605784536,35.,43.9937759547244));
#7369=CARTESIAN_POINT('Ctrl Pts',(-1.83560605784536,35.,37.0008534541443));
#7370=CARTESIAN_POINT('Ctrl Pts',(-1.83560605784536,35.,30.));
#7371=CARTESIAN_POINT('Ctrl Pts',(-1.20914581904087,34.8807245127738,51.0000006501177));
#7372=CARTESIAN_POINT('Ctrl Pts',(-1.20914581904087,34.8807245127738,43.9937759547244));
#7373=CARTESIAN_POINT('Ctrl Pts',(-1.20914581904087,34.8807245127738,37.0008534541443));
#7374=CARTESIAN_POINT('Ctrl Pts',(-1.20914581904087,34.8807245127738,30.));
#7375=CARTESIAN_POINT('Ctrl Pts',(-0.455340235533083,34.2924542918181,51.0000006501177));
#7376=CARTESIAN_POINT('Ctrl Pts',(-0.455340235533083,34.2924542918181,43.9937759547244));
#7377=CARTESIAN_POINT('Ctrl Pts',(-0.455340235533083,34.2924542918181,37.0008534541443));
#7378=CARTESIAN_POINT('Ctrl Pts',(-0.455340235533083,34.2924542918181,30.));
#7379=CARTESIAN_POINT('Ctrl Pts',(-0.065997741473231,33.5498558092142,51.0000006501177));
#7380=CARTESIAN_POINT('Ctrl Pts',(-0.065997741473231,33.5498558092142,43.9937759547244));
#7381=CARTESIAN_POINT('Ctrl Pts',(-0.065997741473231,33.5498558092142,37.0008534541443));
#7382=CARTESIAN_POINT('Ctrl Pts',(-0.065997741473231,33.5498558092142,30.));
#7383=CARTESIAN_POINT('Ctrl Pts',(0.,33.0929653707261,51.0000006501177));
#7384=CARTESIAN_POINT('Ctrl Pts',(0.,33.0929653707261,43.9937759547244));
#7385=CARTESIAN_POINT('Ctrl Pts',(0.,33.0929653707261,37.0008534541443));
#7386=CARTESIAN_POINT('Ctrl Pts',(0.,33.0929653707261,30.));
#7387=CARTESIAN_POINT('Ctrl Pts',(0.,32.8786796564404,51.0000006501177));
#7388=CARTESIAN_POINT('Ctrl Pts',(0.,32.8786796564404,43.9937759547244));
#7389=CARTESIAN_POINT('Ctrl Pts',(0.,32.8786796564404,37.0008534541443));
#7390=CARTESIAN_POINT('Ctrl Pts',(0.,32.8786796564404,30.));
#7391=CARTESIAN_POINT('',(0.,32.8786796564404,30.));
#7392=CARTESIAN_POINT('',(-2.12132034355964,35.,30.));
#7393=CARTESIAN_POINT('Ctrl Pts',(0.,32.8786796564404,30.));
#7394=CARTESIAN_POINT('Ctrl Pts',(0.,33.0929653707261,30.));
#7395=CARTESIAN_POINT('Ctrl Pts',(-0.0329988707366155,33.3214105899701,
30.));
#7396=CARTESIAN_POINT('Ctrl Pts',(-0.107899680213901,33.5470229719827,30.));
#7397=CARTESIAN_POINT('Ctrl Pts',(-0.182800489691187,33.7726353539953,30.));
#7398=CARTESIAN_POINT('Ctrl Pts',(-0.299603237909142,33.9954148987765,30.));
#7399=CARTESIAN_POINT('Ctrl Pts',(-0.454454811586546,34.1914763527892,30.));
#7400=CARTESIAN_POINT('Ctrl Pts',(-0.660923576489751,34.452891624806,30.));
#7401=CARTESIAN_POINT('Ctrl Pts',(-0.935034697765309,34.6668080687899,30.));
#7402=CARTESIAN_POINT('Ctrl Pts',(-1.22870531810421,34.8035851625884,30.));
#7403=CARTESIAN_POINT('Ctrl Pts',(-1.52237593844311,34.9403622563869,30.));
#7404=CARTESIAN_POINT('Ctrl Pts',(-1.83560605784536,35.,30.));
#7405=CARTESIAN_POINT('Ctrl Pts',(-2.12132034355964,35.,30.));
#7406=CARTESIAN_POINT('',(-2.12132034355964,35.,51.0000006501177));
#7407=CARTESIAN_POINT('Ctrl Pts',(-2.12132034355964,35.,30.));
#7408=CARTESIAN_POINT('Ctrl Pts',(-2.12132034355964,35.,37.0008534541443));
#7409=CARTESIAN_POINT('Ctrl Pts',(-2.12132034355964,35.,43.9937759547244));
#7410=CARTESIAN_POINT('Ctrl Pts',(-2.12132034355964,35.,51.0000006501177));
#7411=CARTESIAN_POINT('',(0.,32.8786796564404,51.0000006501177));
#7412=CARTESIAN_POINT('Ctrl Pts',(-2.12132034355964,35.,51.0000006501177));
#7413=CARTESIAN_POINT('Ctrl Pts',(-1.83560605784536,35.,51.0000006501177));
#7414=CARTESIAN_POINT('Ctrl Pts',(-1.20914581904087,34.8807245127738,51.0000006501177));
#7415=CARTESIAN_POINT('Ctrl Pts',(-0.455340235533083,34.2924542918181,51.0000006501177));
#7416=CARTESIAN_POINT('Ctrl Pts',(-0.065997741473231,33.5498558092142,51.0000006501177));
#7417=CARTESIAN_POINT('Ctrl Pts',(0.,33.0929653707261,51.0000006501177));
#7418=CARTESIAN_POINT('Ctrl Pts',(0.,32.8786796564404,51.0000006501177));
#7419=CARTESIAN_POINT('Ctrl Pts',(0.,32.8786796564404,51.0000006501177));
#7420=CARTESIAN_POINT('Ctrl Pts',(0.,32.8786796564404,43.9937759547244));
#7421=CARTESIAN_POINT('Ctrl Pts',(0.,32.8786796564404,37.0008534541443));
#7422=CARTESIAN_POINT('Ctrl Pts',(0.,32.8786796564404,30.));
#7423=CARTESIAN_POINT('Ctrl Pts',(0.,32.8786796564404,51.0000006501177));
#7424=CARTESIAN_POINT('Ctrl Pts',(0.,32.8786796564404,51.197241629744));
#7425=CARTESIAN_POINT('Ctrl Pts',(0.,32.7177646664625,51.6577375903093));
#7426=CARTESIAN_POINT('Ctrl Pts',(0.,32.2629836704437,51.8786803201109));
#7427=CARTESIAN_POINT('Ctrl Pts',(0.,31.9999999547173,51.8786803065581));
#7428=CARTESIAN_POINT('Ctrl Pts',(-3.73831537781851E-17,33.1643939421546,
51.0000006501177));
#7429=CARTESIAN_POINT('Ctrl Pts',(-3.73831537781851E-17,33.1643939421547,
51.2609089327107));
#7430=CARTESIAN_POINT('Ctrl Pts',(-9.25965981612066E-17,32.9508157063449,
51.8707913380558));
#7431=CARTESIAN_POINT('Ctrl Pts',(3.73831537781852E-17,32.3478720188586,
52.1643946101999));
#7432=CARTESIAN_POINT('Ctrl Pts',(3.73831537781851E-17,31.9999999399931,
52.1643945922723));
#7433=CARTESIAN_POINT('Ctrl Pts',(-0.119275961933236,33.7908552904515,51.0000006501177));
#7434=CARTESIAN_POINT('Ctrl Pts',(-0.119275961933236,33.7908552904515,51.4020865730021));
#7435=CARTESIAN_POINT('Ctrl Pts',(-0.119275961933236,33.4629527404772,52.3406964768753));
#7436=CARTESIAN_POINT('Ctrl Pts',(-0.119275961933235,32.5361057932183,52.7908559681974));
#7437=CARTESIAN_POINT('Ctrl Pts',(-0.119275961933235,31.9999999077085,52.7908559405692));
#7438=CARTESIAN_POINT('Ctrl Pts',(-0.707545825143674,34.5446601624604,51.0000006501177));
#7439=CARTESIAN_POINT('Ctrl Pts',(-0.707545825143674,34.5446601624604,51.5711387670255));
#7440=CARTESIAN_POINT('Ctrl Pts',(-0.707545825143674,34.0785969586992,52.9046828234336));
#7441=CARTESIAN_POINT('Ctrl Pts',(-0.707545825143674,32.7615050310335,53.5446608518222));
#7442=CARTESIAN_POINT('Ctrl Pts',(-0.707545825143674,31.9999998688612,53.5446608125781));
#7443=CARTESIAN_POINT('Ctrl Pts',(-1.45014420226184,34.9340027685158,51.0000006501176));
#7444=CARTESIAN_POINT('Ctrl Pts',(-1.45014420226184,34.9340027685159,51.658581172531));
#7445=CARTESIAN_POINT('Ctrl Pts',(-1.45014420226184,34.3966708419147,53.1962044391584));
#7446=CARTESIAN_POINT('Ctrl Pts',(-1.45014420226184,32.8780929976815,53.934003463886));
#7447=CARTESIAN_POINT('Ctrl Pts',(-1.45014420226184,31.9999998487964,53.9340034186335));
#7448=CARTESIAN_POINT('Ctrl Pts',(-1.90703462927393,35.,51.0000006501176));
#7449=CARTESIAN_POINT('Ctrl Pts',(-1.90703462927393,35.,51.6734462278452));
#7450=CARTESIAN_POINT('Ctrl Pts',(-1.90703462927393,34.4506183606249,53.2456947831434));
#7451=CARTESIAN_POINT('Ctrl Pts',(-1.90703462927393,32.8979127471959,54.0000006963915));
#7452=CARTESIAN_POINT('Ctrl Pts',(-1.90703462927393,31.9999998453953,54.0000006501177));
#7453=CARTESIAN_POINT('Ctrl Pts',(-2.12132034355964,35.,51.0000006501176));
#7454=CARTESIAN_POINT('Ctrl Pts',(-2.12132034355964,35.,51.6734234778136));
#7455=CARTESIAN_POINT('Ctrl Pts',(-2.12132034355964,34.4506018588285,53.2456550317936));
#7456=CARTESIAN_POINT('Ctrl Pts',(-2.12132034355964,32.8978824143115,54.00000069639));
#7457=CARTESIAN_POINT('Ctrl Pts',(-2.12132034355964,31.9999998453953,54.0000006501177));
#7458=CARTESIAN_POINT('',(-2.12132034355964,31.9999998453953,54.0000006501177));
#7459=CARTESIAN_POINT('',(0.,31.9999999547173,51.8786803065581));
#7460=CARTESIAN_POINT('Ctrl Pts',(-2.12132034355964,31.9999998453953,54.0000006501177));
#7461=CARTESIAN_POINT('Ctrl Pts',(-1.90703462927393,31.9999998453953,54.0000006501177));
#7462=CARTESIAN_POINT('Ctrl Pts',(-1.45014420226184,31.9999998487964,53.9340034186335));
#7463=CARTESIAN_POINT('Ctrl Pts',(-0.707545825143674,31.9999998688612,53.5446608125781));
#7464=CARTESIAN_POINT('Ctrl Pts',(-0.119275961933235,31.9999999077085,52.7908559405692));
#7465=CARTESIAN_POINT('Ctrl Pts',(3.73831537781851E-17,31.9999999399931,
52.1643945922723));
#7466=CARTESIAN_POINT('Ctrl Pts',(0.,31.9999999547173,51.8786803065581));
#7467=CARTESIAN_POINT('Ctrl Pts',(0.,31.9999999547173,51.8786803065581));
#7468=CARTESIAN_POINT('Ctrl Pts',(0.,32.2629836704437,51.8786803201109));
#7469=CARTESIAN_POINT('Ctrl Pts',(0.,32.7177646664625,51.6577375903093));
#7470=CARTESIAN_POINT('Ctrl Pts',(0.,32.8786796564404,51.197241629744));
#7471=CARTESIAN_POINT('Ctrl Pts',(0.,32.8786796564404,51.0000006501177));
#7472=CARTESIAN_POINT('Ctrl Pts',(-2.12132034355964,35.,51.0000006501176));
#7473=CARTESIAN_POINT('Ctrl Pts',(-2.12132034355964,35.,51.6734234778136));
#7474=CARTESIAN_POINT('Ctrl Pts',(-2.12132034355964,34.4506018588285,53.2456550317936));
#7475=CARTESIAN_POINT('Ctrl Pts',(-2.12132034355964,32.8978824143115,54.00000069639));
#7476=CARTESIAN_POINT('Ctrl Pts',(-2.12132034355964,31.9999998453953,54.0000006501177));
#7477=CARTESIAN_POINT('Ctrl Pts',(-2.12132034355964,19.3800314873921,54.));
#7478=CARTESIAN_POINT('Ctrl Pts',(-2.12132034355964,23.5890030900407,54.0000002168252));
#7479=CARTESIAN_POINT('Ctrl Pts',(-2.12132034355964,27.7896866308398,54.0000004332234));
#7480=CARTESIAN_POINT('Ctrl Pts',(-2.12132034355964,31.9999998454164,54.0000006501177));
#7481=CARTESIAN_POINT('Ctrl Pts',(-1.83560605784536,19.3800314873921,54.));
#7482=CARTESIAN_POINT('Ctrl Pts',(-1.83560605784536,23.5890030900407,54.0000002168252));
#7483=CARTESIAN_POINT('Ctrl Pts',(-1.83560605784536,27.7896866308398,54.0000004332234));
#7484=CARTESIAN_POINT('Ctrl Pts',(-1.83560605784536,31.9999998454164,54.0000006501177));
#7485=CARTESIAN_POINT('Ctrl Pts',(-1.20914581904101,19.3800314935366,53.8807245127739));
#7486=CARTESIAN_POINT('Ctrl Pts',(-1.20914581904101,23.5890030961852,53.880724729599));
#7487=CARTESIAN_POINT('Ctrl Pts',(-1.20914581904101,27.7896866369843,53.8807249459973));
#7488=CARTESIAN_POINT('Ctrl Pts',(-1.20914581904101,31.9999998515609,53.8807251628916));
#7489=CARTESIAN_POINT('Ctrl Pts',(-0.455340235533132,19.3800315238413,53.2924542918181));
#7490=CARTESIAN_POINT('Ctrl Pts',(-0.455340235533132,23.5890031264899,53.2924545086433));
#7491=CARTESIAN_POINT('Ctrl Pts',(-0.455340235533132,27.789686667289,53.2924547250415));
#7492=CARTESIAN_POINT('Ctrl Pts',(-0.455340235533132,31.9999998818656,53.2924549419358));
#7493=CARTESIAN_POINT('Ctrl Pts',(-0.0659977414732951,19.3800315620963,
52.5498558092142));
#7494=CARTESIAN_POINT('Ctrl Pts',(-0.0659977414732951,23.5890031647449,
52.5498560260394));
#7495=CARTESIAN_POINT('Ctrl Pts',(-0.0659977414732951,27.789686705544,52.5498562424376));
#7496=CARTESIAN_POINT('Ctrl Pts',(-0.0659977414732951,31.9999999201206,
52.5498564593319));
#7497=CARTESIAN_POINT('Ctrl Pts',(0.,19.380031585633,52.0929653707261));
#7498=CARTESIAN_POINT('Ctrl Pts',(0.,23.5890031882816,52.0929655875513));
#7499=CARTESIAN_POINT('Ctrl Pts',(0.,27.7896867290807,52.0929658039495));
#7500=CARTESIAN_POINT('Ctrl Pts',(0.,31.9999999436573,52.0929660208438));
#7501=CARTESIAN_POINT('Ctrl Pts',(0.,19.3800315966719,51.8786796564404));
#7502=CARTESIAN_POINT('Ctrl Pts',(0.,23.5890031993205,51.8786798732655));
#7503=CARTESIAN_POINT('Ctrl Pts',(0.,27.7896867401197,51.8786800896638));
#7504=CARTESIAN_POINT('Ctrl Pts',(0.,31.9999999546962,51.8786803065581));
#7505=CARTESIAN_POINT('',(-2.12132034355964,19.3800314873921,54.));
#7506=CARTESIAN_POINT('',(0.,19.3800315966719,51.8786796564404));
#7507=CARTESIAN_POINT('Ctrl Pts',(-2.12132034355964,19.3800314873921,54.));
#7508=CARTESIAN_POINT('Ctrl Pts',(-1.83560605784536,19.3800314873921,54.));
#7509=CARTESIAN_POINT('Ctrl Pts',(-1.20914581904101,19.3800314935366,53.8807245127739));
#7510=CARTESIAN_POINT('Ctrl Pts',(-0.455340235533132,19.3800315238413,53.2924542918181));
#7511=CARTESIAN_POINT('Ctrl Pts',(-0.0659977414732951,19.3800315620963,
52.5498558092142));
#7512=CARTESIAN_POINT('Ctrl Pts',(0.,19.380031585633,52.0929653707261));
#7513=CARTESIAN_POINT('Ctrl Pts',(0.,19.3800315966719,51.8786796564404));
#7514=CARTESIAN_POINT('Ctrl Pts',(0.,19.3800315966719,51.8786796564404));
#7515=CARTESIAN_POINT('Ctrl Pts',(0.,23.5890031993205,51.8786798732655));
#7516=CARTESIAN_POINT('Ctrl Pts',(0.,27.7896867401197,51.8786800896638));
#7517=CARTESIAN_POINT('Ctrl Pts',(0.,31.9999999546962,51.8786803065581));
#7518=CARTESIAN_POINT('Ctrl Pts',(-2.12132034355964,31.9999998454164,54.0000006501177));
#7519=CARTESIAN_POINT('Ctrl Pts',(-2.12132034355964,27.7896866308398,54.0000004332234));
#7520=CARTESIAN_POINT('Ctrl Pts',(-2.12132034355964,23.5890030900407,54.0000002168252));
#7521=CARTESIAN_POINT('Ctrl Pts',(-2.12132034355964,19.3800314873921,54.));
#7522=CARTESIAN_POINT('Ctrl Pts',(-2.12132034355964,17.1834464391567,55.8134832037256));
#7523=CARTESIAN_POINT('Ctrl Pts',(-2.12132034355964,17.2948185578093,55.2359166572309));
#7524=CARTESIAN_POINT('Ctrl Pts',(-2.12132034355964,17.9085541458132,54.3129857845921));
#7525=CARTESIAN_POINT('Ctrl Pts',(-2.12132034355964,18.9389109206226,53.9999999944698));
#7526=CARTESIAN_POINT('Ctrl Pts',(-2.12132034355964,19.3800315154375,54.));
#7527=CARTESIAN_POINT('Ctrl Pts',(-1.83560605784536,17.1834464391567,55.8134832037256));
#7528=CARTESIAN_POINT('Ctrl Pts',(-1.83560605784536,17.2948351576842,55.2358305716603));
#7529=CARTESIAN_POINT('Ctrl Pts',(-1.83560605784536,17.9084593986477,54.3129449535617));
#7530=CARTESIAN_POINT('Ctrl Pts',(-1.83560605784536,18.9388451721502,53.999999994469));
#7531=CARTESIAN_POINT('Ctrl Pts',(-1.83560605784536,19.3800315154375,54.));
#7532=CARTESIAN_POINT('Ctrl Pts',(-1.20915886354306,17.0663340027465,55.7909004204208));
#7533=CARTESIAN_POINT('Ctrl Pts',(-1.20915886354306,17.1836140170936,55.182696018109));
#7534=CARTESIAN_POINT('Ctrl Pts',(-1.20915886354306,17.830272469493,54.2104767085283));
#7535=CARTESIAN_POINT('Ctrl Pts',(-1.20915886354306,18.9155110398637,53.8807301117093));
#7536=CARTESIAN_POINT('Ctrl Pts',(-1.20915886354306,19.3800315169327,53.8807301175329));
#7537=CARTESIAN_POINT('Ctrl Pts',(-0.455344835080339,16.4887007002353,55.6795154292099));
#7538=CARTESIAN_POINT('Ctrl Pts',(-0.455344835080338,16.6352946696137,54.9192912936266));
#7539=CARTESIAN_POINT('Ctrl Pts',(-0.455344835080339,17.4431682391696,53.7044423926936));
#7540=CARTESIAN_POINT('Ctrl Pts',(-0.455344835080339,18.7994048849769,53.2924556433277));
#7541=CARTESIAN_POINT('Ctrl Pts',(-0.455344835080339,19.3800315243078,53.2924556506069));
#7542=CARTESIAN_POINT('Ctrl Pts',(-0.0660036833952015,15.7595336759884,
55.5389102005399));
#7543=CARTESIAN_POINT('Ctrl Pts',(-0.0660036833952008,15.9431143315799,
54.5868761857799));
#7544=CARTESIAN_POINT('Ctrl Pts',(-0.0660036833952016,16.9546119118218,
53.0657000116183));
#7545=CARTESIAN_POINT('Ctrl Pts',(-0.0660036833952013,18.6529087225342,
52.5498558976328));
#7546=CARTESIAN_POINT('Ctrl Pts',(-0.0660036833952013,19.3800315336176,
52.5498559067486));
#7547=CARTESIAN_POINT('Ctrl Pts',(-5.60747306672777E-17,15.3109077300283,
55.4524016892915));
#7548=CARTESIAN_POINT('Ctrl Pts',(1.86449826034637E-16,15.5172134263537,
54.3825175029234));
#7549=CARTESIAN_POINT('Ctrl Pts',(-9.24282552765687E-17,16.6542024147445,
52.6727855991653));
#7550=CARTESIAN_POINT('Ctrl Pts',(3.84627697622366E-25,18.5628998139399,
52.0929653604819));
#7551=CARTESIAN_POINT('Ctrl Pts',(0.,19.3800315393455,52.0929653707261));
#7552=CARTESIAN_POINT('Ctrl Pts',(0.,15.1004981817938,55.411828430134));
#7553=CARTESIAN_POINT('Ctrl Pts',(0.,15.3174807618546,54.2865748125202));
#7554=CARTESIAN_POINT('Ctrl Pts',(0.,16.513201315358,52.4884594099794));
#7555=CARTESIAN_POINT('Ctrl Pts',(0.,18.5206110161515,51.878679645666));
#7556=CARTESIAN_POINT('Ctrl Pts',(0.,19.380031542032,51.8786796564404));
#7557=CARTESIAN_POINT('',(-2.12132034355964,17.1834464391567,55.8134832037256));
#7558=CARTESIAN_POINT('',(0.,15.1004981817938,55.411828430134));
#7559=CARTESIAN_POINT('Ctrl Pts',(-2.12132034355964,17.1834464391567,55.8134832037256));
#7560=CARTESIAN_POINT('Ctrl Pts',(-1.83560605784536,17.1834464391567,55.8134832037256));
#7561=CARTESIAN_POINT('Ctrl Pts',(-1.20915886354306,17.0663340027465,55.7909004204208));
#7562=CARTESIAN_POINT('Ctrl Pts',(-0.455344835080339,16.4887007002353,55.6795154292099));
#7563=CARTESIAN_POINT('Ctrl Pts',(-0.0660036833952015,15.7595336759884,
55.5389102005399));
#7564=CARTESIAN_POINT('Ctrl Pts',(-5.60747306672777E-17,15.3109077300283,
55.4524016892915));
#7565=CARTESIAN_POINT('Ctrl Pts',(0.,15.1004981817938,55.411828430134));
#7566=CARTESIAN_POINT('Ctrl Pts',(0.,15.1004981817938,55.411828430134));
#7567=CARTESIAN_POINT('Ctrl Pts',(0.,15.3174807618546,54.2865748125202));
#7568=CARTESIAN_POINT('Ctrl Pts',(0.,16.513201315358,52.4884594099794));
#7569=CARTESIAN_POINT('Ctrl Pts',(0.,18.5206110161515,51.878679645666));
#7570=CARTESIAN_POINT('Ctrl Pts',(0.,19.380031542032,51.8786796564404));
#7571=CARTESIAN_POINT('Ctrl Pts',(-2.12132034355964,19.3800314873921,54.));
#7572=CARTESIAN_POINT('Ctrl Pts',(-2.12132034355964,18.9389109019061,54.0000000001552));
#7573=CARTESIAN_POINT('Ctrl Pts',(-2.12132034355964,17.9085541402389,54.3129857929746));
#7574=CARTESIAN_POINT('Ctrl Pts',(-2.12132034355964,17.2948185578093,55.2359166572309));
#7575=CARTESIAN_POINT('Ctrl Pts',(-2.12132034355964,17.1834464391567,55.8134832037256));
#7576=CARTESIAN_POINT('Ctrl Pts',(0.,15.1004981817938,55.411828430134));
#7577=CARTESIAN_POINT('Ctrl Pts',(0.,14.7181964939568,57.3944131940254));
#7578=CARTESIAN_POINT('Ctrl Pts',(0.,13.1646620788738,61.2084161039849));
#7579=CARTESIAN_POINT('Ctrl Pts',(0.,8.80253592739979,65.5998831653219));
#7580=CARTESIAN_POINT('Ctrl Pts',(0.,3.09380188060513,67.9778956726815));
#7581=CARTESIAN_POINT('Ctrl Pts',(0.,-3.09300712501298,67.9763940235175));
#7582=CARTESIAN_POINT('Ctrl Pts',(0.,-8.8047766566707,65.6006044096256));
#7583=CARTESIAN_POINT('Ctrl Pts',(0.,-13.1629136545454,61.2080147890074));
#7584=CARTESIAN_POINT('Ctrl Pts',(0.,-14.7181965532993,57.3944130163886));
#7585=CARTESIAN_POINT('Ctrl Pts',(0.,-15.1004982173208,55.4118282458939));
#7586=CARTESIAN_POINT('Ctrl Pts',(0.,15.3810442461065,55.4659261090107));
#7587=CARTESIAN_POINT('Ctrl Pts',(0.,14.9916917803054,57.4850756211365));
#7588=CARTESIAN_POINT('Ctrl Pts',(7.09861723931544E-17,13.4088733048439,
61.3703002831808));
#7589=CARTESIAN_POINT('Ctrl Pts',(-4.54970976055E-17,8.96607423593895,65.8431115317411));
#7590=CARTESIAN_POINT('Ctrl Pts',(1.74366918355959E-17,3.15118170663562,
68.2651806906037));
#7591=CARTESIAN_POINT('Ctrl Pts',(-1.82945629040309E-17,-3.1504293962536,
68.2638373394039));
#7592=CARTESIAN_POINT('Ctrl Pts',(3.3983836790065E-17,-8.96823047064176,
65.8437131532327));
#7593=CARTESIAN_POINT('Ctrl Pts',(-7.83977616403127E-17,-13.4072864799347,
61.3698938985013));
#7594=CARTESIAN_POINT('Ctrl Pts',(0.,-14.9916918407472,57.4850754401985));
#7595=CARTESIAN_POINT('Ctrl Pts',(0.,-15.3810442822936,55.4659259213477));
#7596=CARTESIAN_POINT('Ctrl Pts',(-0.119271769306436,15.9961640790422,55.584539625384));
#7597=CARTESIAN_POINT('Ctrl Pts',(-0.119271769306436,15.5911770229754,57.6847688225764));
#7598=CARTESIAN_POINT('Ctrl Pts',(-0.119271769306436,13.9455752772508,61.7249266531959));
#7599=CARTESIAN_POINT('Ctrl Pts',(-0.119271769306436,9.3246466833128,66.3769129854858));
#7600=CARTESIAN_POINT('Ctrl Pts',(-0.119271769306436,3.27732498131823,68.8959971218407));
#7601=CARTESIAN_POINT('Ctrl Pts',(-0.119271769306436,-3.27647243413541,
68.8943717375029));
#7602=CARTESIAN_POINT('Ctrl Pts',(-0.119271769306436,-9.32704380078624,
66.3777017761324));
#7603=CARTESIAN_POINT('Ctrl Pts',(-0.119271769306436,-13.9436870123243,
61.7245010904894));
#7604=CARTESIAN_POINT('Ctrl Pts',(-0.119271769306436,-15.5911770858384,
57.6847686344034));
#7605=CARTESIAN_POINT('Ctrl Pts',(-0.119271769306436,-15.9961641166764,
55.584539430216));
#7606=CARTESIAN_POINT('Ctrl Pts',(-0.707544802288016,16.7363397346456,55.7272676477045));
#7607=CARTESIAN_POINT('Ctrl Pts',(-0.707544802288016,16.3126311460358,57.9245851559279));
#7608=CARTESIAN_POINT('Ctrl Pts',(-0.707544802288016,14.5907371808805,62.1518158552224));
#7609=CARTESIAN_POINT('Ctrl Pts',(-0.707544802288017,9.75611724712778,67.0189745688111));
#7610=CARTESIAN_POINT('Ctrl Pts',(-0.707544802288016,3.42893923539705,69.6545789430513));
#7611=CARTESIAN_POINT('Ctrl Pts',(-0.707544802288016,-3.42806716335815,
69.6529431938856));
#7612=CARTESIAN_POINT('Ctrl Pts',(-0.707544802288016,-9.75858135999868,
67.0197535318122));
#7613=CARTESIAN_POINT('Ctrl Pts',(-0.707544802288017,-14.5888291335536,
62.1513714318578));
#7614=CARTESIAN_POINT('Ctrl Pts',(-0.707544802288016,-16.3126312118065,
57.9245849590475));
#7615=CARTESIAN_POINT('Ctrl Pts',(-0.707544802288016,-16.7363397740212,
55.7272674435056));
#7616=CARTESIAN_POINT('Ctrl Pts',(-1.45014411828137,17.1186386297034,55.8009863181496));
#7617=CARTESIAN_POINT('Ctrl Pts',(-1.45014411828137,16.685246310872,58.0485228460791));
#7618=CARTESIAN_POINT('Ctrl Pts',(-1.45014411828137,14.9240622829779,62.3722774913806));
#7619=CARTESIAN_POINT('Ctrl Pts',(-1.45014411828137,9.97897084989204,67.3506383401551));
#7620=CARTESIAN_POINT('Ctrl Pts',(-1.45014411828137,3.50727446402829,70.0464587202164));
#7621=CARTESIAN_POINT('Ctrl Pts',(-1.45014411828137,-3.50637674445434,70.044766966671));
#7622=CARTESIAN_POINT('Ctrl Pts',(-1.45014411828137,-9.98150387523715,67.3514484132735));
#7623=CARTESIAN_POINT('Ctrl Pts',(-1.45014411828137,-14.9220912218402,62.3718226774245));
#7624=CARTESIAN_POINT('Ctrl Pts',(-1.45014411828137,-16.6852463781453,58.0485226447015));
#7625=CARTESIAN_POINT('Ctrl Pts',(-1.45014411828137,-17.1186386699785,55.8009861092864));
#7626=CARTESIAN_POINT('Ctrl Pts',(-1.90703462927393,17.1834464391567,55.8134832037256));
#7627=CARTESIAN_POINT('Ctrl Pts',(-1.90703462927393,16.7484079032003,58.0695568767787));
#7628=CARTESIAN_POINT('Ctrl Pts',(-1.90703462927393,14.9806009228527,62.4096420606667));
#7629=CARTESIAN_POINT('Ctrl Pts',(-1.90703462927393,10.0167493251233,67.4068756953095));
#7630=CARTESIAN_POINT('Ctrl Pts',(-1.90703462927393,3.520562743488,70.1129149705606));
#7631=CARTESIAN_POINT('Ctrl Pts',(-1.90703462927393,-3.51965558020761,70.1111971380699));
#7632=CARTESIAN_POINT('Ctrl Pts',(-1.90703462927393,-10.0193052668116,67.4077028909198));
#7633=CARTESIAN_POINT('Ctrl Pts',(-1.90703462927393,-14.9786018920781,62.4091852727419));
#7634=CARTESIAN_POINT('Ctrl Pts',(-1.90703462927393,-16.7484079707286,58.0695566746388));
#7635=CARTESIAN_POINT('Ctrl Pts',(-1.90703462927393,-17.1834464795842,55.8134829940716));
#7636=CARTESIAN_POINT('Ctrl Pts',(-2.12132034355964,17.1834464391567,55.8134832037256));
#7637=CARTESIAN_POINT('Ctrl Pts',(-2.12132034355964,16.748410422632,58.0695438112154));
#7638=CARTESIAN_POINT('Ctrl Pts',(-2.12132034355964,14.9805829581613,62.4096466298823));
#7639=CARTESIAN_POINT('Ctrl Pts',(-2.12132034355964,10.0167493029862,67.4068684519269));
#7640=CARTESIAN_POINT('Ctrl Pts',(-2.12132034355964,3.52055794906399,70.1129017271154));
#7641=CARTESIAN_POINT('Ctrl Pts',(-2.12132034355964,-3.5196535656466,70.1111929419039));
#7642=CARTESIAN_POINT('Ctrl Pts',(-2.12132034355964,-10.0192991163067,67.4076891839791));
#7643=CARTESIAN_POINT('Ctrl Pts',(-2.12132034355964,-14.9785933578555,62.4091899579011));
#7644=CARTESIAN_POINT('Ctrl Pts',(-2.12132034355964,-16.7484104901601,58.0695436090755));
#7645=CARTESIAN_POINT('Ctrl Pts',(-2.12132034355964,-17.1834464795842,55.8134829940716));
#7646=CARTESIAN_POINT('',(-2.12132034355964,-17.1834464391567,55.8134832037256));
#7647=CARTESIAN_POINT('',(0.,-15.1004981817938,55.411828430134));
#7648=CARTESIAN_POINT('Ctrl Pts',(-2.12132034355964,-17.1834464795842,55.8134829940716));
#7649=CARTESIAN_POINT('Ctrl Pts',(-1.90703462927393,-17.1834464795842,55.8134829940716));
#7650=CARTESIAN_POINT('Ctrl Pts',(-1.45014411828137,-17.1186386699785,55.8009861092864));
#7651=CARTESIAN_POINT('Ctrl Pts',(-0.707544802288016,-16.7363397740212,
55.7272674435056));
#7652=CARTESIAN_POINT('Ctrl Pts',(-0.119271769306436,-15.9961641166764,
55.584539430216));
#7653=CARTESIAN_POINT('Ctrl Pts',(0.,-15.3810442822936,55.4659259213477));
#7654=CARTESIAN_POINT('Ctrl Pts',(0.,-15.1004982173208,55.4118282458939));
#7655=CARTESIAN_POINT('Ctrl Pts',(0.,-15.1004981462668,55.411828614374));
#7656=CARTESIAN_POINT('Ctrl Pts',(0.,-14.7181964569451,57.3944132526519));
#7657=CARTESIAN_POINT('Ctrl Pts',(0.,-13.1629135645458,61.2080148797186));
#7658=CARTESIAN_POINT('Ctrl Pts',(0.,-8.8047766566707,65.6006044096256));
#7659=CARTESIAN_POINT('Ctrl Pts',(0.,-3.09300712501298,67.9763940235175));
#7660=CARTESIAN_POINT('Ctrl Pts',(0.,3.09380188060513,67.9778956726815));
#7661=CARTESIAN_POINT('Ctrl Pts',(0.,8.80253592739979,65.5998831653219));
#7662=CARTESIAN_POINT('Ctrl Pts',(0.,13.1646620788738,61.2084161039849));
#7663=CARTESIAN_POINT('Ctrl Pts',(0.,14.7181964939568,57.3944131940254));
#7664=CARTESIAN_POINT('Ctrl Pts',(0.,15.1004981817938,55.411828430134));
#7665=CARTESIAN_POINT('Ctrl Pts',(-2.12132034355964,17.1834464391567,55.8134832037256));
#7666=CARTESIAN_POINT('Ctrl Pts',(-2.12132034355964,16.748410422632,58.0695438112154));
#7667=CARTESIAN_POINT('Ctrl Pts',(-2.12132034355964,14.9805829581613,62.4096466298823));
#7668=CARTESIAN_POINT('Ctrl Pts',(-2.12132034355964,10.0167493029862,67.4068684519269));
#7669=CARTESIAN_POINT('Ctrl Pts',(-2.12132034355964,3.52055794906399,70.1129017271154));
#7670=CARTESIAN_POINT('Ctrl Pts',(-2.12132034355964,-3.5196535656466,70.1111929419039));
#7671=CARTESIAN_POINT('Ctrl Pts',(-2.12132034355964,-10.0192991163067,67.4076891839791));
#7672=CARTESIAN_POINT('Ctrl Pts',(-2.12132034355964,-14.9785932554414,62.4091900611248));
#7673=CARTESIAN_POINT('Ctrl Pts',(-2.12132034355964,-16.748410380515,58.0695438779288));
#7674=CARTESIAN_POINT('Ctrl Pts',(-2.12132034355964,-17.1834463987291,55.8134834133795));
#7675=CARTESIAN_POINT('Ctrl Pts',(-2.12132034355964,-19.3800314873921,54.));
#7676=CARTESIAN_POINT('Ctrl Pts',(-2.12132034355964,-18.9389108965653,54.));
#7677=CARTESIAN_POINT('Ctrl Pts',(-2.12132034355964,-17.9085541350523,54.3129857971382));
#7678=CARTESIAN_POINT('Ctrl Pts',(-2.12132034355964,-17.2948185567905,55.2359166625147));
#7679=CARTESIAN_POINT('Ctrl Pts',(-2.12132034355964,-17.1834464391567,55.8134832037256));
#7680=CARTESIAN_POINT('Ctrl Pts',(-1.83560605784536,-19.3800314873921,54.));
#7681=CARTESIAN_POINT('Ctrl Pts',(-1.83560605784536,-18.9388451480935,54.));
#7682=CARTESIAN_POINT('Ctrl Pts',(-1.83560605784536,-17.9084593878876,54.3129449661094));
#7683=CARTESIAN_POINT('Ctrl Pts',(-1.83560605784536,-17.2948351566652,55.2358305769448));
#7684=CARTESIAN_POINT('Ctrl Pts',(-1.83560605784536,-17.1834464391567,55.8134832037256));
#7685=CARTESIAN_POINT('Ctrl Pts',(-1.20915886354309,-19.3800314873921,53.8807301175329));
#7686=CARTESIAN_POINT('Ctrl Pts',(-1.20915886354309,-18.9155110145227,53.8807301175329));
#7687=CARTESIAN_POINT('Ctrl Pts',(-1.20915886354309,-17.8302724581569,54.2104767217406));
#7688=CARTESIAN_POINT('Ctrl Pts',(-1.20915886354309,-17.1836140160207,55.1826960236731));
#7689=CARTESIAN_POINT('Ctrl Pts',(-1.20915886354309,-17.0663340027465,55.7909004204208));
#7690=CARTESIAN_POINT('Ctrl Pts',(-0.45534483508035,-19.3800314873921,53.2924556506069));
#7691=CARTESIAN_POINT('Ctrl Pts',(-0.45534483508035,-18.7994048533105,53.2924556506069));
#7692=CARTESIAN_POINT('Ctrl Pts',(-0.455344835080351,-17.443168225005,53.7044424092076));
#7693=CARTESIAN_POINT('Ctrl Pts',(-0.45534483508035,-16.6352946682726,54.9192913005814));
#7694=CARTESIAN_POINT('Ctrl Pts',(-0.45534483508035,-16.4887007002353,55.6795154292099));
#7695=CARTESIAN_POINT('Ctrl Pts',(-0.0660036833952163,-19.3800314873921,
52.5498559067486));
#7696=CARTESIAN_POINT('Ctrl Pts',(-0.0660036833952163,-18.6529086828825,
52.5498559067486));
#7697=CARTESIAN_POINT('Ctrl Pts',(-0.0660036833952168,-16.9546118940859,
53.0657000322986));
#7698=CARTESIAN_POINT('Ctrl Pts',(-0.0660036833952163,-15.9431143299004,
54.5868761944894));
#7699=CARTESIAN_POINT('Ctrl Pts',(-0.0660036833952163,-15.7595336759884,
55.5389102005399));
#7700=CARTESIAN_POINT('Ctrl Pts',(0.,-19.3800314873921,52.0929653707261));
#7701=CARTESIAN_POINT('Ctrl Pts',(1.70917049581581E-32,-18.562899769374,
52.0929653707261));
#7702=CARTESIAN_POINT('Ctrl Pts',(-1.87111548691343E-16,-16.6542023948098,
52.672785622406));
#7703=CARTESIAN_POINT('Ctrl Pts',(-2.42907311579532E-18,-15.5172134244663,
54.382517512711));
#7704=CARTESIAN_POINT('Ctrl Pts',(0.,-15.3109077300283,55.4524016892915));
#7705=CARTESIAN_POINT('Ctrl Pts',(0.,-19.3800314873921,51.8786796564404));
#7706=CARTESIAN_POINT('Ctrl Pts',(0.,-18.5206109692815,51.8786796564404));
#7707=CARTESIAN_POINT('Ctrl Pts',(0.,-16.5132012943929,52.4884594344227));
#7708=CARTESIAN_POINT('Ctrl Pts',(0.,-15.3174807598696,54.2865748228144));
#7709=CARTESIAN_POINT('Ctrl Pts',(0.,-15.1004981817938,55.411828430134));
#7710=CARTESIAN_POINT('',(-2.12132034355964,-19.3800314873921,54.));
#7711=CARTESIAN_POINT('',(0.,-19.3800314873921,51.8786796564404));
#7712=CARTESIAN_POINT('Ctrl Pts',(-2.12132034355964,-19.3800314873921,54.));
#7713=CARTESIAN_POINT('Ctrl Pts',(-1.83560605784536,-19.3800314873921,54.));
#7714=CARTESIAN_POINT('Ctrl Pts',(-1.20915886354309,-19.3800314873921,53.8807301175329));
#7715=CARTESIAN_POINT('Ctrl Pts',(-0.45534483508035,-19.3800314873921,53.2924556506069));
#7716=CARTESIAN_POINT('Ctrl Pts',(-0.0660036833952163,-19.3800314873921,
52.5498559067486));
#7717=CARTESIAN_POINT('Ctrl Pts',(0.,-19.3800314873921,52.0929653707261));
#7718=CARTESIAN_POINT('Ctrl Pts',(0.,-19.3800314873921,51.8786796564404));
#7719=CARTESIAN_POINT('Ctrl Pts',(0.,-19.3800314873921,51.8786796564404));
#7720=CARTESIAN_POINT('Ctrl Pts',(0.,-18.5206109692815,51.8786796564404));
#7721=CARTESIAN_POINT('Ctrl Pts',(0.,-16.5132012943929,52.4884594344227));
#7722=CARTESIAN_POINT('Ctrl Pts',(0.,-15.3174807598696,54.2865748228144));
#7723=CARTESIAN_POINT('Ctrl Pts',(0.,-15.1004981817938,55.411828430134));
#7724=CARTESIAN_POINT('Ctrl Pts',(-2.12132034355964,-17.1834464391567,55.8134832037256));
#7725=CARTESIAN_POINT('Ctrl Pts',(-2.12132034355964,-17.2948185567905,55.2359166625147));
#7726=CARTESIAN_POINT('Ctrl Pts',(-2.12132034355964,-17.9085541350523,54.3129857971382));
#7727=CARTESIAN_POINT('Ctrl Pts',(-2.12132034355964,-18.9389108965653,54.));
#7728=CARTESIAN_POINT('Ctrl Pts',(-2.12132034355964,-19.3800314873921,54.));
#7729=CARTESIAN_POINT('Ctrl Pts',(0.,-19.380031542032,51.8786796564404));
#7730=CARTESIAN_POINT('Ctrl Pts',(0.,-23.5890031639361,51.8786798732655));
#7731=CARTESIAN_POINT('Ctrl Pts',(0.,-27.7896867219788,51.8786800896638));
#7732=CARTESIAN_POINT('Ctrl Pts',(0.,-31.9999999547658,51.8786803065581));
#7733=CARTESIAN_POINT('Ctrl Pts',(0.,-19.3800315273134,52.1643939421546));
#7734=CARTESIAN_POINT('Ctrl Pts',(0.,-23.5890031492176,52.1643941589798));
#7735=CARTESIAN_POINT('Ctrl Pts',(0.,-27.7896867072603,52.164394375378));
#7736=CARTESIAN_POINT('Ctrl Pts',(0.,-31.9999999400472,52.1643945922723));
#7737=CARTESIAN_POINT('Ctrl Pts',(-0.119275487226149,-19.3800314950413,
52.790854180959));
#7738=CARTESIAN_POINT('Ctrl Pts',(-0.119275487226149,-23.5890031169454,
52.7908543977842));
#7739=CARTESIAN_POINT('Ctrl Pts',(-0.119275487226149,-27.7896866749881,
52.7908546141824));
#7740=CARTESIAN_POINT('Ctrl Pts',(-0.119275487226149,-31.9999999077751,
52.7908548310767));
#7741=CARTESIAN_POINT('Ctrl Pts',(-0.707545708181871,-19.380031456209,53.5446597644669));
#7742=CARTESIAN_POINT('Ctrl Pts',(-0.707545708181871,-23.5890030781132,
53.544659981292));
#7743=CARTESIAN_POINT('Ctrl Pts',(-0.707545708181871,-27.7896866361559,
53.5446601976903));
#7744=CARTESIAN_POINT('Ctrl Pts',(-0.707545708181871,-31.9999998689428,
53.5446604145846));
#7745=CARTESIAN_POINT('Ctrl Pts',(-1.45014419078584,-19.380031436152,53.9340022585267));
#7746=CARTESIAN_POINT('Ctrl Pts',(-1.45014419078584,-23.5890030580562,53.9340024753519));
#7747=CARTESIAN_POINT('Ctrl Pts',(-1.45014419078584,-27.7896866160989,53.9340026917501));
#7748=CARTESIAN_POINT('Ctrl Pts',(-1.45014419078584,-31.9999998488858,53.9340029086444));
#7749=CARTESIAN_POINT('Ctrl Pts',(-1.90703462927393,-19.3800314327522,54.));
#7750=CARTESIAN_POINT('Ctrl Pts',(-1.90703462927393,-23.5890030546563,54.0000002168252));
#7751=CARTESIAN_POINT('Ctrl Pts',(-1.90703462927393,-27.789686612699,54.0000004332234));
#7752=CARTESIAN_POINT('Ctrl Pts',(-1.90703462927393,-31.999999845486,54.0000006501177));
#7753=CARTESIAN_POINT('Ctrl Pts',(-2.12132034355964,-19.3800314327522,54.));
#7754=CARTESIAN_POINT('Ctrl Pts',(-2.12132034355964,-23.5890030546563,54.0000002168252));
#7755=CARTESIAN_POINT('Ctrl Pts',(-2.12132034355964,-27.789686612699,54.0000004332234));
#7756=CARTESIAN_POINT('Ctrl Pts',(-2.12132034355964,-31.999999845486,54.0000006501177));
#7757=CARTESIAN_POINT('',(-2.12132034355964,-31.999999845486,54.0000006501177));
#7758=CARTESIAN_POINT('',(0.,-31.9999999547658,51.8786803065581));
#7759=CARTESIAN_POINT('Ctrl Pts',(-2.12132034355964,-31.999999845486,54.0000006501177));
#7760=CARTESIAN_POINT('Ctrl Pts',(-1.90703462927393,-31.999999845486,54.0000006501177));
#7761=CARTESIAN_POINT('Ctrl Pts',(-1.45014419078584,-31.9999998488858,53.9340029086444));
#7762=CARTESIAN_POINT('Ctrl Pts',(-0.707545708181871,-31.9999998689428,
53.5446604145846));
#7763=CARTESIAN_POINT('Ctrl Pts',(-0.119275487226149,-31.9999999077751,
52.7908548310767));
#7764=CARTESIAN_POINT('Ctrl Pts',(0.,-31.9999999400472,52.1643945922723));
#7765=CARTESIAN_POINT('Ctrl Pts',(0.,-31.9999999547658,51.8786803065581));
#7766=CARTESIAN_POINT('Ctrl Pts',(0.,-31.9999999547658,51.8786803065581));
#7767=CARTESIAN_POINT('Ctrl Pts',(0.,-27.7896867219788,51.8786800896638));
#7768=CARTESIAN_POINT('Ctrl Pts',(0.,-23.5890031639361,51.8786798732655));
#7769=CARTESIAN_POINT('Ctrl Pts',(0.,-19.380031542032,51.8786796564404));
#7770=CARTESIAN_POINT('Ctrl Pts',(-2.12132034355964,-19.3800314873921,54.));
#7771=CARTESIAN_POINT('Ctrl Pts',(-2.12132034355964,-23.5890030910112,54.0000002168252));
#7772=CARTESIAN_POINT('Ctrl Pts',(-2.12132034355964,-27.7896866309181,54.0000004332234));
#7773=CARTESIAN_POINT('Ctrl Pts',(-2.12132034355964,-31.999999845486,54.0000006501177));
#7774=CARTESIAN_POINT('Ctrl Pts',(0.,-31.9999999547548,51.8786803065581));
#7775=CARTESIAN_POINT('Ctrl Pts',(0.,-32.1972377415442,51.8786803167143));
#7776=CARTESIAN_POINT('Ctrl Pts',(0.,-32.6577149440455,51.7177834826772));
#7777=CARTESIAN_POINT('Ctrl Pts',(0.,-32.8786796564446,51.2629886229218));
#7778=CARTESIAN_POINT('Ctrl Pts',(0.,-32.8786796564404,51.0000006501034));
#7779=CARTESIAN_POINT('Ctrl Pts',(0.,-31.9999999400427,52.1643945922723));
#7780=CARTESIAN_POINT('Ctrl Pts',(0.,-32.2609039991848,52.1643946057069));
#7781=CARTESIAN_POINT('Ctrl Pts',(-9.08192836805913E-17,-32.8707615917812,
51.9508403862498));
#7782=CARTESIAN_POINT('Ctrl Pts',(3.52858375230007E-16,-33.1643939421603,
51.3478783602006));
#7783=CARTESIAN_POINT('Ctrl Pts',(0.,-33.1643939421546,51.0000006500987));
#7784=CARTESIAN_POINT('Ctrl Pts',(-0.119275961933235,-31.9999999077849,
52.7908559405692));
#7785=CARTESIAN_POINT('Ctrl Pts',(-0.119275961933235,-32.4020793219062,
52.7908559612732));
#7786=CARTESIAN_POINT('Ctrl Pts',(-0.119275961933236,-33.3406509864574,
52.4629904231461));
#7787=CARTESIAN_POINT('Ctrl Pts',(-0.119275961933234,-33.7908552904603,
51.5361152139003));
#7788=CARTESIAN_POINT('Ctrl Pts',(-0.119275961933235,-33.7908552904515,
51.0000006500885));
#7789=CARTESIAN_POINT('Ctrl Pts',(-0.707545825143674,-31.9999998689697,
53.5446608125781));
#7790=CARTESIAN_POINT('Ctrl Pts',(-0.707545825143674,-32.5711287405834,
53.5446608419868));
#7791=CARTESIAN_POINT('Ctrl Pts',(-0.707545825143674,-33.9046184804968,
53.078650211204));
#7792=CARTESIAN_POINT('Ctrl Pts',(-0.707545825143673,-34.5446601624728,
51.7615181392383));
#7793=CARTESIAN_POINT('Ctrl Pts',(-0.707545825143674,-34.5446601624604,
51.0000006500762));
#7794=CARTESIAN_POINT('Ctrl Pts',(-1.45014420226184,-31.9999998489216,53.9340034186335));
#7795=CARTESIAN_POINT('Ctrl Pts',(-1.45014420226184,-32.6585697105674,53.9340034525448));
#7796=CARTESIAN_POINT('Ctrl Pts',(-1.45014420226184,-34.1961303447082,53.3967321479677));
#7797=CARTESIAN_POINT('Ctrl Pts',(-1.45014420226184,-34.9340027685302,51.8781080132318));
#7798=CARTESIAN_POINT('Ctrl Pts',(-1.45014420226184,-34.9340027685158,51.0000006500698));
#7799=CARTESIAN_POINT('Ctrl Pts',(-1.90703462927393,-31.9999998455233,54.0000006501177));
#7800=CARTESIAN_POINT('Ctrl Pts',(-1.90703462927393,-32.6734345218553,54.0000006847944));
#7801=CARTESIAN_POINT('Ctrl Pts',(-1.90703462927393,-34.2456190309428,53.4506810357792));
#7802=CARTESIAN_POINT('Ctrl Pts',(-1.90703462927393,-35.0000000000147,51.8979280869818));
#7803=CARTESIAN_POINT('Ctrl Pts',(-1.90703462927393,-35.,51.0000006500687));
#7804=CARTESIAN_POINT('Ctrl Pts',(-2.12132034355964,-31.9999998455233,54.0000006501177));
#7805=CARTESIAN_POINT('Ctrl Pts',(-2.12132034355964,-32.673411772192,54.0000006847932));
#7806=CARTESIAN_POINT('Ctrl Pts',(-2.12132034355964,-34.2455792821355,53.4506645318811));
#7807=CARTESIAN_POINT('Ctrl Pts',(-2.12132034355964,-35.0000000000147,51.8978977536063));
#7808=CARTESIAN_POINT('Ctrl Pts',(-2.12132034355964,-35.,51.0000006500687));
#7809=CARTESIAN_POINT('',(-2.12132034355964,-35.,51.0000006500688));
#7810=CARTESIAN_POINT('',(0.,-32.8786796564404,51.0000006501034));
#7811=CARTESIAN_POINT('Ctrl Pts',(-2.12132034355964,-35.,51.0000006500687));
#7812=CARTESIAN_POINT('Ctrl Pts',(-1.90703462927393,-35.,51.0000006500687));
#7813=CARTESIAN_POINT('Ctrl Pts',(-1.45014420226184,-34.9340027685158,51.0000006500698));
#7814=CARTESIAN_POINT('Ctrl Pts',(-0.707545825143674,-34.5446601624604,
51.0000006500762));
#7815=CARTESIAN_POINT('Ctrl Pts',(-0.119275961933235,-33.7908552904515,
51.0000006500885));
#7816=CARTESIAN_POINT('Ctrl Pts',(0.,-33.1643939421546,51.0000006500987));
#7817=CARTESIAN_POINT('Ctrl Pts',(0.,-32.8786796564404,51.0000006501034));
#7818=CARTESIAN_POINT('Ctrl Pts',(0.,-32.8786796564404,51.0000006501034));
#7819=CARTESIAN_POINT('Ctrl Pts',(0.,-32.8786796564446,51.2629886229218));
#7820=CARTESIAN_POINT('Ctrl Pts',(0.,-32.6577149440455,51.7177834826772));
#7821=CARTESIAN_POINT('Ctrl Pts',(0.,-32.1972377415442,51.8786803167143));
#7822=CARTESIAN_POINT('Ctrl Pts',(0.,-31.9999999547548,51.8786803065581));
#7823=CARTESIAN_POINT('Ctrl Pts',(-2.12132034355964,-31.9999998455233,54.0000006501177));
#7824=CARTESIAN_POINT('Ctrl Pts',(-2.12132034355964,-32.673411772192,54.0000006847932));
#7825=CARTESIAN_POINT('Ctrl Pts',(-2.12132034355964,-34.2455792821355,53.4506645318811));
#7826=CARTESIAN_POINT('Ctrl Pts',(-2.12132034355964,-35.0000000000147,51.8978977536063));
#7827=CARTESIAN_POINT('Ctrl Pts',(-2.12132034355964,-35.,51.0000006500687));
#7828=CARTESIAN_POINT('Ctrl Pts',(0.,-32.8786796564404,51.0000006500861));
#7829=CARTESIAN_POINT('Ctrl Pts',(0.,-32.8786796564404,43.9937759550453));
#7830=CARTESIAN_POINT('Ctrl Pts',(0.,-32.8786796564404,37.0008502462934));
#7831=CARTESIAN_POINT('Ctrl Pts',(0.,-32.8786796564404,30.));
#7832=CARTESIAN_POINT('Ctrl Pts',(0.,-33.1643939421546,51.0000006500861));
#7833=CARTESIAN_POINT('Ctrl Pts',(0.,-33.1643939421546,43.9937759550453));
#7834=CARTESIAN_POINT('Ctrl Pts',(0.,-33.1643939421546,37.0008502462934));
#7835=CARTESIAN_POINT('Ctrl Pts',(0.,-33.1643939421546,30.));
#7836=CARTESIAN_POINT('Ctrl Pts',(-0.119275487226208,-33.7908541809591,
51.0000006500861));
#7837=CARTESIAN_POINT('Ctrl Pts',(-0.119275487226208,-33.7908541809591,
43.9937759550453));
#7838=CARTESIAN_POINT('Ctrl Pts',(-0.119275487226208,-33.7908541809591,
37.0008502462934));
#7839=CARTESIAN_POINT('Ctrl Pts',(-0.119275487226208,-33.7908541809591,
30.));
#7840=CARTESIAN_POINT('Ctrl Pts',(-0.707545708181886,-34.5446597644669,
51.0000006500861));
#7841=CARTESIAN_POINT('Ctrl Pts',(-0.707545708181886,-34.5446597644669,
43.9937759550453));
#7842=CARTESIAN_POINT('Ctrl Pts',(-0.707545708181886,-34.5446597644669,
37.0008502462934));
#7843=CARTESIAN_POINT('Ctrl Pts',(-0.707545708181886,-34.5446597644669,
30.));
#7844=CARTESIAN_POINT('Ctrl Pts',(-1.45014419078585,-34.9340022585268,51.0000006500861));
#7845=CARTESIAN_POINT('Ctrl Pts',(-1.45014419078585,-34.9340022585268,43.9937759550453));
#7846=CARTESIAN_POINT('Ctrl Pts',(-1.45014419078585,-34.9340022585268,37.0008502462934));
#7847=CARTESIAN_POINT('Ctrl Pts',(-1.45014419078585,-34.9340022585268,30.));
#7848=CARTESIAN_POINT('Ctrl Pts',(-1.90703462927393,-35.,51.0000006500861));
#7849=CARTESIAN_POINT('Ctrl Pts',(-1.90703462927393,-35.,43.9937759550453));
#7850=CARTESIAN_POINT('Ctrl Pts',(-1.90703462927393,-35.,37.0008502462934));
#7851=CARTESIAN_POINT('Ctrl Pts',(-1.90703462927393,-35.,30.));
#7852=CARTESIAN_POINT('Ctrl Pts',(-2.12132034355964,-35.,51.0000006500861));
#7853=CARTESIAN_POINT('Ctrl Pts',(-2.12132034355964,-35.,43.9937759550453));
#7854=CARTESIAN_POINT('Ctrl Pts',(-2.12132034355964,-35.,37.0008502462934));
#7855=CARTESIAN_POINT('Ctrl Pts',(-2.12132034355964,-35.,30.));
#7856=CARTESIAN_POINT('',(-2.12132034355964,-35.,30.));
#7857=CARTESIAN_POINT('',(0.,-32.8786796564404,30.));
#7858=CARTESIAN_POINT('Ctrl Pts',(-2.12132034355964,-35.,30.));
#7859=CARTESIAN_POINT('Ctrl Pts',(-1.90703462927393,-35.,30.));
#7860=CARTESIAN_POINT('Ctrl Pts',(-1.67858941002989,-34.9670011292634,30.));
#7861=CARTESIAN_POINT('Ctrl Pts',(-1.45297702801727,-34.8921003197861,30.));
#7862=CARTESIAN_POINT('Ctrl Pts',(-1.22736464600466,-34.8171995103088,30.));
#7863=CARTESIAN_POINT('Ctrl Pts',(-1.00458510122347,-34.7003967620909,30.));
#7864=CARTESIAN_POINT('Ctrl Pts',(-0.808523647210829,-34.5455451884135,
30.));
#7865=CARTESIAN_POINT('Ctrl Pts',(-0.547108375193974,-34.3390764235102,
30.));
#7866=CARTESIAN_POINT('Ctrl Pts',(-0.333191931210091,-34.0649653022347,
30.));
#7867=CARTESIAN_POINT('Ctrl Pts',(-0.196414837411598,-33.7712946818958,
30.));
#7868=CARTESIAN_POINT('Ctrl Pts',(-0.0596377436131043,-33.4776240615569,
30.));
#7869=CARTESIAN_POINT('Ctrl Pts',(0.,-33.1643939421546,30.));
#7870=CARTESIAN_POINT('Ctrl Pts',(0.,-32.8786796564404,30.));
#7871=CARTESIAN_POINT('Ctrl Pts',(0.,-32.8786796564404,30.));
#7872=CARTESIAN_POINT('Ctrl Pts',(0.,-32.8786796564404,37.0008502462934));
#7873=CARTESIAN_POINT('Ctrl Pts',(0.,-32.8786796564404,43.9937759550453));
#7874=CARTESIAN_POINT('Ctrl Pts',(0.,-32.8786796564404,51.0000006500861));
#7875=CARTESIAN_POINT('Ctrl Pts',(-2.12132034355964,-35.,51.0000006500861));
#7876=CARTESIAN_POINT('Ctrl Pts',(-2.12132034355964,-35.,43.9937759550453));
#7877=CARTESIAN_POINT('Ctrl Pts',(-2.12132034355964,-35.,37.0008502462934));
#7878=CARTESIAN_POINT('Ctrl Pts',(-2.12132034355964,-35.,30.));
#7879=CARTESIAN_POINT('Origin',(0.,-35.,30.));
#7880=CARTESIAN_POINT('',(-40.,-35.,31.));
#7881=CARTESIAN_POINT('',(-20.,-35.,31.));
#7882=CARTESIAN_POINT('',(-40.1715728752538,-35.,30.));
#7883=CARTESIAN_POINT('Origin',(-43.,-35.,31.));
#7884=CARTESIAN_POINT('',(0.,-35.,30.));
#7885=CARTESIAN_POINT('',(0.,-35.,51.0000006501177));
#7886=CARTESIAN_POINT('Origin',(0.,-32.,51.0000006501177));
#7887=CARTESIAN_POINT('',(0.,-31.999999845455,54.0000006501177));
#7888=CARTESIAN_POINT('Origin',(0.,-31.999999845455,54.0000006501177));
#7889=CARTESIAN_POINT('',(0.,-19.3800314873921,54.));
#7890=CARTESIAN_POINT('Origin',(0.,-19.3800314873921,56.2370505521246));
#7891=CARTESIAN_POINT('',(0.,-17.1834460733662,55.8134831331902));
#7892=CARTESIAN_POINT('Origin',(0.,0.,52.500000372529));
#7893=CARTESIAN_POINT('',(0.,17.1834464391567,55.8134832037256));
#7894=CARTESIAN_POINT('Origin',(0.,19.3800314873921,56.2370505521246));
#7895=CARTESIAN_POINT('',(0.,19.3800314873921,54.));
#7896=CARTESIAN_POINT('Origin',(0.,19.3800314873921,54.));
#7897=CARTESIAN_POINT('',(0.,31.999999845455,54.0000006501177));
#7898=CARTESIAN_POINT('Origin',(0.,32.,51.0000006501177));
#7899=CARTESIAN_POINT('',(-40.,35.,51.0000006501177));
#7900=CARTESIAN_POINT('',(0.,35.,51.0000006501177));
#7901=CARTESIAN_POINT('',(-40.,34.9999541371497,51.0165890494702));
#7902=CARTESIAN_POINT('Origin',(-40.,32.,51.0000006501177));
#7903=CARTESIAN_POINT('',(0.,34.9999541371497,51.0165890496373));
#7904=CARTESIAN_POINT('Origin',(0.,35.,51.0000006501177));
#7905=CARTESIAN_POINT('',(-40.1715728752538,35.,30.));
#7906=CARTESIAN_POINT('',(0.,35.,30.));
#7907=CARTESIAN_POINT('',(-40.,35.,31.));
#7908=CARTESIAN_POINT('Origin',(-43.,35.,31.));
#7909=CARTESIAN_POINT('',(-40.,35.,41.0000003250588));
#7910=CARTESIAN_POINT('Origin',(0.,35.,30.));
#7911=CARTESIAN_POINT('',(0.,12.5,30.));
#7912=CARTESIAN_POINT('',(0.,12.5,30.));
#7913=CARTESIAN_POINT('',(-40.1715728752538,12.5,30.));
#7914=CARTESIAN_POINT('',(0.,12.5,30.));
#7915=CARTESIAN_POINT('',(-40.1715728752538,-12.5,30.));
#7916=CARTESIAN_POINT('Origin',(-40.,-35.0001000000116,74.8720791843357));
#7917=CARTESIAN_POINT('',(-40.,-35.0001000000116,74.8720791843357));
#7918=CARTESIAN_POINT('',(-40.,-35.0001000000116,74.8720791843357));
#7919=CARTESIAN_POINT('',(-40.,-35.0001000000116,74.8720791843357));
#7920=CARTESIAN_POINT('Origin',(-40.,34.9998994784478,74.8720791843357));
#7921=CARTESIAN_POINT('',(-40.,34.9998994784478,74.8720791843345));
#7922=CARTESIAN_POINT('',(-40.,34.9998994784478,74.8720791843345));
#7923=CARTESIAN_POINT('',(-40.,-35.0001000000116,74.8720791843357));
#7924=CARTESIAN_POINT('Origin',(-40.,34.9999541371497,51.0165890494702));
#7925=CARTESIAN_POINT('',(-40.,34.9998994784478,74.8720791843345));
#7926=CARTESIAN_POINT('Origin',(-40.,-12.5,31.));
#7927=CARTESIAN_POINT('',(-40.,-12.5,31.));
#7928=CARTESIAN_POINT('Origin',(-43.,-12.5,31.));
#7929=CARTESIAN_POINT('',(-43.,12.5,28.));
#7930=CARTESIAN_POINT('Origin',(-43.,12.5,31.));
#7931=CARTESIAN_POINT('',(-43.,-12.5,28.));
#7932=CARTESIAN_POINT('',(-43.,-12.5,28.));
#7933=CARTESIAN_POINT('',(-40.1715728752538,-12.5,30.));
#7934=CARTESIAN_POINT('Origin',(-43.,-12.5,31.));
#7935=CARTESIAN_POINT('',(-40.1715728752538,-12.5,30.));
#7936=CARTESIAN_POINT('Origin',(-54.1954416479917,-12.5,28.));
#7937=CARTESIAN_POINT('',(-54.1954416479917,12.5,28.));
#7938=CARTESIAN_POINT('',(-27.0977208239958,12.5,28.));
#7939=CARTESIAN_POINT('',(-54.1954416479917,-12.5,28.));
#7940=CARTESIAN_POINT('',(-54.1954416479917,-12.5,28.));
#7941=CARTESIAN_POINT('',(-27.0977208239958,-12.5,28.));
#7942=CARTESIAN_POINT('Origin',(-54.1954416479917,-12.5,25.));
#7943=CARTESIAN_POINT('',(-57.0932191268589,12.5,25.7764571353076));
#7944=CARTESIAN_POINT('Origin',(-54.1954416479917,12.5,25.));
#7945=CARTESIAN_POINT('',(-57.0932191268589,-12.5,25.7764571353076));
#7946=CARTESIAN_POINT('',(-57.0932191268589,-12.5,25.7764571353076));
#7947=CARTESIAN_POINT('Origin',(-54.1954416479917,-12.5,25.));
#7948=CARTESIAN_POINT('Origin',(-59.9807621135332,-12.5,15.));
#7949=CARTESIAN_POINT('',(-57.3012701892219,12.5,25.));
#7950=CARTESIAN_POINT('',(-56.0967875173176,12.5,29.4951905283833));
#7951=CARTESIAN_POINT('',(-57.3012701892219,7.,25.));
#7952=CARTESIAN_POINT('',(-57.3012701892219,0.,25.));
#7953=CARTESIAN_POINT('',(-59.9807621135332,7.,15.));
#7954=CARTESIAN_POINT('',(-56.7217875173176,7.,27.1626587736527));
#7955=CARTESIAN_POINT('',(-59.9807621135332,-7.,15.));
#7956=CARTESIAN_POINT('',(-59.9807621135332,-12.5,15.));
#7957=CARTESIAN_POINT('',(-57.3012701892219,-7.,25.));
#7958=CARTESIAN_POINT('',(-57.9717875173176,-7.,22.4975952641916));
#7959=CARTESIAN_POINT('',(-57.3012701892219,-12.5,25.));
#7960=CARTESIAN_POINT('',(-57.3012701892219,-9.75,25.));
#7961=CARTESIAN_POINT('',(-56.7217875173176,-12.5,27.1626587736527));
#7962=CARTESIAN_POINT('Origin',(0.,-12.5,30.));
#7963=CARTESIAN_POINT('',(0.,-12.5,30.));
#7964=CARTESIAN_POINT('',(0.,-12.5,30.));
#7965=CARTESIAN_POINT('',(0.,-12.5,30.));
#7966=CARTESIAN_POINT('Origin',(0.,-12.5,25.));
#7967=CARTESIAN_POINT('',(0.,-12.5,25.));
#7968=CARTESIAN_POINT('',(0.,-12.5,25.));
#7969=CARTESIAN_POINT('',(0.,-12.5,25.));
#7970=CARTESIAN_POINT('Origin',(0.,-7.,25.));
#7971=CARTESIAN_POINT('',(0.,-7.,25.));
#7972=CARTESIAN_POINT('',(0.,-7.,25.));
#7973=CARTESIAN_POINT('',(0.,-7.,25.));
#7974=CARTESIAN_POINT('Origin',(0.,-7.,15.));
#7975=CARTESIAN_POINT('',(0.,-7.,15.));
#7976=CARTESIAN_POINT('',(0.,-7.,15.));
#7977=CARTESIAN_POINT('',(0.,-7.,15.));
#7978=CARTESIAN_POINT('Origin',(-8.41954981558864,-5.55111512312578E-15,
66.0000009834766));
#7979=CARTESIAN_POINT('',(-8.,-1.00000000000001,66.0000009834766));
#7980=CARTESIAN_POINT('Origin',(-8.,-5.55111512312578E-15,66.0000009834766));
#7981=CARTESIAN_POINT('',(-8.83909963117728,-5.55111512312578E-15,66.0000009834766));
#7982=CARTESIAN_POINT('',(-8.41954981558864,-0.500000000000006,66.0000009834766));
#7983=CARTESIAN_POINT('Origin',(-4.,-5.55111512312578E-15,66.0000009834766));
#7984=CARTESIAN_POINT('',(0.,-1.00000000000001,66.0000009834766));
#7985=CARTESIAN_POINT('Origin',(0.,-5.55111512312578E-15,66.0000009834766));
#7986=CARTESIAN_POINT('',(-4.,-1.00000000000001,66.0000009834766));
#7987=CARTESIAN_POINT('Origin',(-10.,0.,52.500000372529));
#7988=CARTESIAN_POINT('',(0.,-9.5,52.500000372529));
#7989=CARTESIAN_POINT('Origin',(0.,0.,52.500000372529));
#7990=CARTESIAN_POINT('',(-20.,-9.5,52.500000372529));
#7991=CARTESIAN_POINT('',(-10.,-9.5,52.500000372529));
#7992=CARTESIAN_POINT('Origin',(-20.,0.,52.500000372529));
#7993=CARTESIAN_POINT('Origin',(-20.,0.,52.500000372529));
#7994=CARTESIAN_POINT('Origin',(0.,12.5,0.));
#7995=CARTESIAN_POINT('',(0.,-12.5,0.));
#7996=CARTESIAN_POINT('',(0.,12.5,1.53080849893419E-15));
#7997=CARTESIAN_POINT('',(0.,-12.5,0.));
#7998=CARTESIAN_POINT('',(-64.,-12.5,0.));
#7999=CARTESIAN_POINT('',(0.,-12.5,0.));
#8000=CARTESIAN_POINT('',(-64.,12.5,1.53080849893419E-15));
#8001=CARTESIAN_POINT('',(-64.,-12.5,0.));
#8002=CARTESIAN_POINT('',(0.,12.5,1.53080849893419E-15));
#8003=CARTESIAN_POINT('Origin',(0.,12.5,15.));
#8004=CARTESIAN_POINT('',(0.,12.5,15.));
#8005=CARTESIAN_POINT('',(0.,12.5,1.53080849893419E-15));
#8006=CARTESIAN_POINT('',(-64.,12.5,15.));
#8007=CARTESIAN_POINT('',(-64.,12.5,1.53080849893419E-15));
#8008=CARTESIAN_POINT('',(0.,12.5,15.));
#8009=CARTESIAN_POINT('Origin',(0.,7.,15.));
#8010=CARTESIAN_POINT('',(0.,7.,15.));
#8011=CARTESIAN_POINT('',(0.,7.,15.));
#8012=CARTESIAN_POINT('',(0.,12.5,15.));
#8013=CARTESIAN_POINT('',(-64.,-12.5,15.));
#8014=CARTESIAN_POINT('',(-64.,-12.5,15.));
#8015=CARTESIAN_POINT('',(0.,-12.5,15.));
#8016=CARTESIAN_POINT('',(0.,-12.5,15.));
#8017=CARTESIAN_POINT('',(0.,-12.5,15.));
#8018=CARTESIAN_POINT('Origin',(0.,7.,25.));
#8019=CARTESIAN_POINT('',(0.,7.,25.));
#8020=CARTESIAN_POINT('',(0.,7.,25.));
#8021=CARTESIAN_POINT('',(0.,7.,15.));
#8022=CARTESIAN_POINT('Origin',(0.,12.5,25.));
#8023=CARTESIAN_POINT('',(0.,12.5,25.));
#8024=CARTESIAN_POINT('',(0.,12.5,25.));
#8025=CARTESIAN_POINT('',(0.,7.,25.));
#8026=CARTESIAN_POINT('Origin',(0.,12.5,30.));
#8027=CARTESIAN_POINT('',(0.,12.5,25.));
#8028=CARTESIAN_POINT('Origin',(0.,-12.5,0.));
#8029=CARTESIAN_POINT('',(0.,-12.5,0.));
#8030=CARTESIAN_POINT('',(-64.,-12.5,0.));
#8031=CARTESIAN_POINT('Origin',(0.,0.,35.0000001862645));
#8032=CARTESIAN_POINT('Origin',(-64.,0.,35.0000001862645));
#8426=UNCERTAINTY_MEASURE_WITH_UNIT(LENGTH_MEASURE(0.01),#8446,
'DISTANCE_ACCURACY_VALUE',
'Maximum model space distance between geometric entities at asserted c
onnectivities');
#8434=UNCERTAINTY_MEASURE_WITH_UNIT(LENGTH_MEASURE(0.01),#8446,
'DISTANCE_ACCURACY_VALUE',
'Maximum model space distance between geometric entities at asserted c
onnectivities');
#8437=(
GEOMETRIC_REPRESENTATION_CONTEXT(3)
GLOBAL_UNCERTAINTY_ASSIGNED_CONTEXT((#8426))
GLOBAL_UNIT_ASSIGNED_CONTEXT((#8446,#8448,#8449))
REPRESENTATION_CONTEXT('','3D')
);
#8445=(
GEOMETRIC_REPRESENTATION_CONTEXT(3)
GLOBAL_UNCERTAINTY_ASSIGNED_CONTEXT((#8434))
GLOBAL_UNIT_ASSIGNED_CONTEXT((#8446,#8448,#8449))
REPRESENTATION_CONTEXT('','3D')
);
#8446=(
LENGTH_UNIT()
NAMED_UNIT(*)
SI_UNIT(.MILLI.,.METRE.)
);
#8448=(
NAMED_UNIT(*)
PLANE_ANGLE_UNIT()
SI_UNIT($,.RADIAN.)
);
#8449=(
NAMED_UNIT(*)
SI_UNIT($,.STERADIAN.)
SOLID_ANGLE_UNIT()
);
#8452=SHAPE_DEFINITION_REPRESENTATION(#8462,#8485);
#8462=PRODUCT_DEFINITION_SHAPE('',$,#8496);
#8485=SHAPE_REPRESENTATION('',(#4284),#8437);
#8493=PRODUCT_DEFINITION_CONTEXT('part definition',#8525,'design');
#8496=PRODUCT_DEFINITION('2026-10-05-01-11-38-185','Configuration 1',#8506,
#8493);
#8506=PRODUCT_DEFINITION_FORMATION('',$,#8529);
#8525=APPLICATION_CONTEXT(
'Core Data for Automotive Mechanical Design Process');
#8526=PRODUCT_CONTEXT('part definition',#8525,'mechanical');
#8529=PRODUCT('2026-10-05-01-11-38-185','Configuration 1',$,(#8526));
#8537=PRESENTATION_STYLE_ASSIGNMENT((#8538));
#8538=SURFACE_STYLE_USAGE(.BOTH.,#8539);
#8539=SURFACE_SIDE_STYLE('',(#8540));
#8540=SURFACE_STYLE_FILL_AREA(#8541);
#8541=FILL_AREA_STYLE('Steel - Satin',(#8542));
#8542=FILL_AREA_STYLE_COLOUR('Steel - Satin',#8543);
#8543=COLOUR_RGB('Steel - Satin', 0.09019608, 0.27058824, 0.51372549);
ENDSEC;
END-ISO-10303-21;
